ISO-10303-21;
HEADER;
/* Generated by software containing ST-Developer
 * from STEP Tools, Inc. (www.steptools.com) 
 */

FILE_DESCRIPTION(
/* description */ ('Independent maintained push-to-latch/pull-to-reset mushroom-operator 
CAD. Two opposed spring-loaded ball detents in turned circular seats b
ias both travel stops; direct normally-closed bridge opens6mm when pre
ssed. Rounded palm/pull rim, captured head screw, removable detent clo
sures, native Coil spring families, insulated shared terminals and ord
inary machining features. Manual geometric states and ideal same-mater
ial spring-energy direction only; no electrical/safety certification, 
force/contact dynamics, wear, load or life rating. Requested blue/gray
 visual palette, not safety identification. External wiring/anchors an
d application engineering omitted.'),
/* implementation_level */ '2;1');

FILE_NAME(
/* name */ 'Socket head cap screw M10x4.step',
/* time_stamp */ '2026-11-08T17:54:26-08:00',
/* author */ (''),
/* organization */ (''),
/* preprocessor_version */ 'ST-DEVELOPER v20.2',
/* originating_system */ 'Autodesk Translation Framework v15.17.0.0',
/* authorisation */ '');

FILE_SCHEMA (('AUTOMOTIVE_DESIGN { 1 0 10303 214 3 1 1 }'));
ENDSEC;

DATA;
#10=MECHANICAL_DESIGN_GEOMETRIC_PRESENTATION_REPRESENTATION('',(#206),#43980);
#150=CONICAL_SURFACE('',#12214,0.45,0.785398163397448);
#172=SHAPE_REPRESENTATION_RELATIONSHIP('SRR','None',#44072,#189);
#189=ADVANCED_BREP_SHAPE_REPRESENTATION('',(#223),#43979);
#206=STYLED_ITEM('',(#44160),#223);
#223=MANIFOLD_SOLID_BREP('Body1',#11247);
#256=B_SPLINE_SURFACE_WITH_KNOTS('',3,3,((#43487,#43488,#43489,#43490,#43491,
#43492,#43493,#43494,#43495,#43496,#43497,#43498,#43499,#43500,#43501,#43502,
#43503,#43504,#43505,#43506,#43507,#43508),(#43509,#43510,#43511,#43512,
#43513,#43514,#43515,#43516,#43517,#43518,#43519,#43520,#43521,#43522,#43523,
#43524,#43525,#43526,#43527,#43528,#43529,#43530),(#43531,#43532,#43533,
#43534,#43535,#43536,#43537,#43538,#43539,#43540,#43541,#43542,#43543,#43544,
#43545,#43546,#43547,#43548,#43549,#43550,#43551,#43552),(#43553,#43554,
#43555,#43556,#43557,#43558,#43559,#43560,#43561,#43562,#43563,#43564,#43565,
#43566,#43567,#43568,#43569,#43570,#43571,#43572,#43573,#43574)),
 .UNSPECIFIED.,.F.,.F.,.F.,(4,4),(4,1,1,1,1,1,1,1,1,1,1,1,1,1,1,1,1,1,1,
4),(0.,0.098669161004507),(11.6147305479243,12.0988438158569,12.5829570837895,
13.5511836196547,14.5194101555198,15.487636691385,16.4558632272502,17.4240897631154,
18.3923162989806,19.3605428348458,20.3287693707109,21.2969959065761,22.2652224424413,
23.2334489783065,24.2016755141717,25.1699020500369,26.138128585902,27.1063551217672,
27.5904683896998,28.0745816576324),.UNSPECIFIED.);
#257=B_SPLINE_SURFACE_WITH_KNOTS('',3,3,((#43680,#43681,#43682,#43683,#43684,
#43685,#43686,#43687,#43688,#43689,#43690,#43691,#43692,#43693,#43694,#43695,
#43696,#43697,#43698,#43699,#43700,#43701,#43702,#43703),(#43704,#43705,
#43706,#43707,#43708,#43709,#43710,#43711,#43712,#43713,#43714,#43715,#43716,
#43717,#43718,#43719,#43720,#43721,#43722,#43723,#43724,#43725,#43726,#43727),
(#43728,#43729,#43730,#43731,#43732,#43733,#43734,#43735,#43736,#43737,
#43738,#43739,#43740,#43741,#43742,#43743,#43744,#43745,#43746,#43747,#43748,
#43749,#43750,#43751),(#43752,#43753,#43754,#43755,#43756,#43757,#43758,
#43759,#43760,#43761,#43762,#43763,#43764,#43765,#43766,#43767,#43768,#43769,
#43770,#43771,#43772,#43773,#43774,#43775)),.UNSPECIFIED.,.F.,.F.,.F.,(4,
4),(4,1,1,1,1,1,1,1,1,1,1,1,1,1,1,1,1,1,1,1,1,4),(0.,0.098669161004507),
(8.30989595155341,8.79743208801023,9.28496822446705,10.2600404973807,11.2351127702943,
12.2101850432079,13.1852573161216,14.1603295890352,15.1354018619488,16.1104741348625,
17.0855464077761,18.0606186806897,19.0356909536033,20.010763226517,20.9858354994306,
21.9609077723442,22.9359800452579,23.9110523181715,24.8861245910851,25.8611968639988,
26.3487330004556,26.8362691369124),.UNSPECIFIED.);
#329=FACE_BOUND('',#1796,.T.);
#330=FACE_BOUND('',#1799,.T.);
#474=PLANE('',#12220);
#475=PLANE('',#12221);
#476=PLANE('',#12222);
#477=PLANE('',#12223);
#478=PLANE('',#12224);
#479=PLANE('',#12225);
#480=PLANE('',#12226);
#481=PLANE('',#12227);
#482=PLANE('',#12231);
#483=PLANE('',#12232);
#1086=FACE_OUTER_BOUND('',#1779,.T.);
#1087=FACE_OUTER_BOUND('',#1780,.T.);
#1088=FACE_OUTER_BOUND('',#1781,.T.);
#1089=FACE_OUTER_BOUND('',#1782,.T.);
#1090=FACE_OUTER_BOUND('',#1783,.T.);
#1091=FACE_OUTER_BOUND('',#1784,.T.);
#1092=FACE_OUTER_BOUND('',#1785,.T.);
#1093=FACE_OUTER_BOUND('',#1786,.T.);
#1094=FACE_OUTER_BOUND('',#1787,.T.);
#1095=FACE_OUTER_BOUND('',#1788,.T.);
#1096=FACE_OUTER_BOUND('',#1789,.T.);
#1097=FACE_OUTER_BOUND('',#1790,.T.);
#1098=FACE_OUTER_BOUND('',#1791,.T.);
#1099=FACE_OUTER_BOUND('',#1792,.T.);
#1100=FACE_OUTER_BOUND('',#1793,.T.);
#1101=FACE_OUTER_BOUND('',#1794,.T.);
#1102=FACE_OUTER_BOUND('',#1795,.T.);
#1103=FACE_OUTER_BOUND('',#1797,.T.);
#1104=FACE_OUTER_BOUND('',#1798,.T.);
#1105=FACE_OUTER_BOUND('',#1800,.T.);
#1779=EDGE_LOOP('',(#10087,#10088,#10089,#10090));
#1780=EDGE_LOOP('',(#10091,#10092,#10093,#10094));
#1781=EDGE_LOOP('',(#10095,#10096,#10097,#10098));
#1782=EDGE_LOOP('',(#10099,#10100,#10101,#10102));
#1783=EDGE_LOOP('',(#10103,#10104,#10105,#10106,#10107,#10108,#10109,#10110));
#1784=EDGE_LOOP('',(#10111,#10112,#10113,#10114,#10115,#10116,#10117,#10118));
#1785=EDGE_LOOP('',(#10119,#10120,#10121,#10122));
#1786=EDGE_LOOP('',(#10123,#10124,#10125,#10126,#10127,#10128,#10129,#10130,
#10131));
#1787=EDGE_LOOP('',(#10132,#10133,#10134,#10135));
#1788=EDGE_LOOP('',(#10136,#10137,#10138,#10139));
#1789=EDGE_LOOP('',(#10140,#10141,#10142,#10143));
#1790=EDGE_LOOP('',(#10144,#10145,#10146,#10147));
#1791=EDGE_LOOP('',(#10148,#10149,#10150,#10151));
#1792=EDGE_LOOP('',(#10152,#10153,#10154,#10155));
#1793=EDGE_LOOP('',(#10156,#10157,#10158,#10159));
#1794=EDGE_LOOP('',(#10160,#10161,#10162,#10163,#10164,#10165));
#1795=EDGE_LOOP('',(#10166));
#1796=EDGE_LOOP('',(#10167,#10168,#10169,#10170));
#1797=EDGE_LOOP('',(#10171,#10172,#10173,#10174));
#1798=EDGE_LOOP('',(#10175));
#1799=EDGE_LOOP('',(#10176,#10177,#10178,#10179,#10180,#10181));
#1800=EDGE_LOOP('',(#10182));
#1985=CIRCLE('',#12209,0.4925);
#1986=CIRCLE('',#12212,0.40705);
#1987=CIRCLE('',#12215,0.4925);
#1988=CIRCLE('',#12216,0.4);
#1989=CIRCLE('',#12218,0.40705);
#1990=CIRCLE('',#12228,0.6);
#1991=CIRCLE('',#12230,0.6);
#2813=B_SPLINE_CURVE_WITH_KNOTS('',3,(#43135,#43136,#43137,#43138,#43139,
#43140,#43141,#43142,#43143,#43144),.UNSPECIFIED.,.F.,.F.,(4,3,3,4),(-4.09323272002468,
-3.87290614346074,-2.90467960759555,-2.06652207565085),.UNSPECIFIED.);
#2814=B_SPLINE_CURVE_WITH_KNOTS('',3,(#43147,#43148,#43149,#43150,#43151,
#43152,#43153,#43154,#43155,#43156),.UNSPECIFIED.,.F.,.F.,(4,3,3,4),(0.,
0.487536136456814,0.97507227291363,1.11488200921596),.UNSPECIFIED.);
#2815=B_SPLINE_CURVE_WITH_KNOTS('',3,(#43161,#43162,#43163,#43164,#43165,
#43166,#43167,#43168,#43169,#43170,#43171,#43172,#43173,#43174,#43175,#43176,
#43177,#43178,#43179,#43180,#43181,#43182),.UNSPECIFIED.,.F.,.F.,(4,3,3,
3,3,3,3,4),(-10.3764180272043,-9.68226535865184,-8.71403882278665,-7.74581228692147,
-6.77758575105629,-5.8093592151911,-4.84113267932592,-4.09323272002468),
 .UNSPECIFIED.);
#2816=B_SPLINE_CURVE_WITH_KNOTS('',3,(#43183,#43184,#43185,#43186,#43187,
#43188,#43189,#43190,#43191,#43192,#43193,#43194,#43195,#43196,#43197,#43198,
#43199,#43200,#43201,#43202,#43203,#43204),.UNSPECIFIED.,.F.,.F.,(4,3,3,
3,3,3,3,4),(1.11488200921596,1.95014454582726,2.92521681874089,3.90028909165452,
4.87536136456815,5.85043363748178,6.82550591039541,7.39806731639555),
 .UNSPECIFIED.);
#2817=B_SPLINE_CURVE_WITH_KNOTS('',3,(#43210,#43211,#43212,#43213,#43214,
#43215,#43216,#43217,#43218,#43219,#43220),.UNSPECIFIED.,.F.,.F.,(4,1,1,
1,1,1,1,1,4),(21.9911485751286,22.2652224424413,23.2334489783065,24.2016755141717,
25.1699020500369,26.138128585902,27.1063551217672,27.5904683896998,28.0745816576324),
 .UNSPECIFIED.);
#2818=B_SPLINE_CURVE_WITH_KNOTS('',3,(#43223,#43224,#43225,#43226,#43227,
#43228,#43229,#43230,#43231),.UNSPECIFIED.,.F.,.F.,(4,1,1,1,1,1,4),(21.9911485751286,
22.9359800452579,23.9110523181715,24.8861245910851,25.8611968639988,26.3487330004556,
26.8362691369124),.UNSPECIFIED.);
#2819=B_SPLINE_CURVE_WITH_KNOTS('',3,(#43236,#43237,#43238,#43239,#43240,
#43241,#43242,#43243,#43244,#43245),.UNSPECIFIED.,.F.,.F.,(4,1,1,1,1,1,
1,4),(15.707963267949,16.4558632272502,17.4240897631154,18.3923162989806,
19.3605428348458,20.3287693707109,21.2969959065761,21.9911485751286),
 .UNSPECIFIED.);
#2820=B_SPLINE_CURVE_WITH_KNOTS('',3,(#43246,#43247,#43248,#43249,#43250,
#43251,#43252,#43253,#43254,#43255,#43256),.UNSPECIFIED.,.F.,.F.,(4,1,1,
1,1,1,1,1,4),(15.707963267949,16.1104741348625,17.0855464077761,18.0606186806897,
19.0356909536033,20.010763226517,20.9858354994306,21.9609077723442,21.9911485751286),
 .UNSPECIFIED.);
#2821=B_SPLINE_CURVE_WITH_KNOTS('',3,(#43259,#43260,#43261,#43262,#43263,
#43264,#43265,#43266,#43267,#43268,#43269,#43270,#43271,#43272,#43273,#43274,
#43275,#43276,#43277,#43278,#43279,#43280,#43281,#43282,#43283,#43284,#43285,
#43286,#43287,#43288,#43289,#43290,#43291,#43292,#43293,#43294,#43295,#43296,
#43297,#43298,#43299,#43300,#43301,#43302,#43303,#43304,#43305,#43306,#43307,
#43308,#43309,#43310,#43311,#43312,#43313,#43314,#43315,#43316,#43317,#43318,
#43319,#43320,#43321,#43322,#43323,#43324,#43325,#43326,#43327,#43328,#43329,
#43330,#43331,#43332,#43333,#43334,#43335,#43336,#43337,#43338,#43339,#43340,
#43341,#43342,#43343,#43344,#43345,#43346,#43347,#43348,#43349,#43350,#43351,
#43352,#43353,#43354,#43355,#43356,#43357,#43358,#43359,#43360,#43361,#43362,
#43363,#43364,#43365,#43366,#43367,#43368,#43369,#43370,#43371,#43372,#43373,
#43374,#43375,#43376,#43377,#43378,#43379,#43380,#43381,#43382,#43383,#43384,
#43385,#43386,#43387,#43388,#43389,#43390,#43391,#43392,#43393,#43394,#43395,
#43396,#43397,#43398,#43399,#43400,#43401,#43402,#43403,#43404,#43405,#43406),
 .UNSPECIFIED.,.F.,.F.,(4,3,3,3,3,3,3,3,3,3,3,3,3,3,3,3,3,3,3,3,3,3,3,3,
3,3,3,3,3,3,3,3,3,3,3,3,3,3,3,3,3,3,3,3,3,3,3,3,3,4),(-2.55484760629189,
-2.48695217528833,-2.44568453284157,-2.42070459558115,-2.35319160200125,
-2.3139257865929,-2.29446012350936,-2.22112134316782,-2.15284489776411,
-2.14778256282628,-2.13140597699043,-2.06209153930656,-2.00885523871797,
-1.98486130911199,-1.96992692853568,-1.89815536257881,-1.83937078561554,
-1.817015847285,-1.80036421341341,-1.72620354597493,-1.67173851911123,-1.64378629426763,
-1.62739425282856,-1.55539099825264,-1.48916408145581,-1.46822556014781,
-1.45145722328267,-1.37758996208556,-1.33403664657543,-1.30743916113377,
-1.29048333106531,-1.2185386082438,-1.1539632168897,-1.12355490177176,-1.10204286950436,
-1.02677942328141,-0.963665843738869,-0.934374946244716,-0.917466118562855,
-0.840611933806436,-0.784435130234986,-0.756523277472602,-0.739287897272494,
-0.66391879015127,-0.595738468922161,-0.571248146417653,-0.555619165378024,
-0.478231758999867,-0.402728776225848,-0.391197505234835),.UNSPECIFIED.);
#2822=B_SPLINE_CURVE_WITH_KNOTS('',3,(#43408,#43409,#43410,#43411,#43412,
#43413,#43414,#43415,#43416,#43417,#43418,#43419,#43420,#43421,#43422,#43423,
#43424,#43425,#43426,#43427,#43428,#43429,#43430,#43431,#43432,#43433,#43434,
#43435,#43436,#43437,#43438,#43439,#43440,#43441,#43442,#43443,#43444,#43445,
#43446,#43447,#43448,#43449,#43450,#43451,#43452,#43453,#43454,#43455,#43456),
 .UNSPECIFIED.,.F.,.F.,(4,3,3,3,3,3,3,3,3,3,3,3,3,3,3,3,4),(-0.691756841576666,
-0.614945525020825,-0.557220644991909,-0.525771290850366,-0.506808473351499,
-0.433893818313954,-0.428434150029101,-0.373272348832725,-0.346954927725707,
-0.325495518311274,-0.254200825411291,-0.207786945243596,-0.17148998018176,
-0.153620305836439,-0.084801943824183,-0.0177085843821423,0.),
 .UNSPECIFIED.);
#2823=B_SPLINE_CURVE_WITH_KNOTS('',3,(#43459,#43460,#43461,#43462,#43463,
#43464,#43465,#43466,#43467,#43468,#43469,#43470,#43471,#43472,#43473,#43474,
#43475,#43476,#43477,#43478,#43479,#43480,#43481,#43482,#43483),
 .UNSPECIFIED.,.F.,.F.,(4,3,3,3,3,3,3,3,4),(-0.391197505234835,-0.376635177103455,
-0.301774337514086,-0.226330753135565,-0.196964234530146,-0.179195669298564,
-0.100760744171276,-0.022735359240347,0.),.UNSPECIFIED.);
#2824=B_SPLINE_CURVE_WITH_KNOTS('',3,(#43576,#43577,#43578,#43579,#43580,
#43581,#43582,#43583,#43584),.UNSPECIFIED.,.F.,.F.,(4,1,1,1,1,1,4),(11.6147305479243,
12.0988438158569,12.5829570837895,13.5511836196547,14.5194101555198,15.487636691385,
15.707963267949),.UNSPECIFIED.);
#2825=B_SPLINE_CURVE_WITH_KNOTS('',3,(#43585,#43586,#43587,#43588,#43589,
#43590,#43591,#43592,#43593,#43594,#43595,#43596,#43597,#43598,#43599,#43600,
#43601,#43602,#43603,#43604,#43605,#43606,#43607,#43608,#43609,#43610,#43611,
#43612,#43613,#43614,#43615,#43616,#43617,#43618,#43619,#43620,#43621,#43622,
#43623,#43624,#43625,#43626,#43627,#43628,#43629,#43630,#43631,#43632,#43633,
#43634,#43635,#43636,#43637,#43638,#43639,#43640,#43641,#43642,#43643,#43644,
#43645,#43646,#43647,#43648),.UNSPECIFIED.,.F.,.F.,(4,3,3,3,3,3,3,3,3,3,
3,3,3,3,3,3,3,3,3,3,3,4),(-0.933975894023133,-0.870172144297646,-0.827170080065546,
-0.803663315340509,-0.727385743658459,-0.693021198251103,-0.668606761857492,
-0.594193624789495,-0.539597646441439,-0.51029826305353,-0.489836959863564,
-0.416327925555324,-0.363092036646369,-0.336301819444199,-0.31659765616087,
-0.24641892633565,-0.203384369919504,-0.167041232727781,-0.150137294418877,
-0.0818130912649662,-0.0151584267138751,0.),.UNSPECIFIED.);
#2826=B_SPLINE_CURVE_WITH_KNOTS('',3,(#43649,#43650,#43651,#43652,#43653,
#43654,#43655,#43656,#43657,#43658,#43659,#43660,#43661,#43662,#43663,#43664,
#43665,#43666,#43667),.UNSPECIFIED.,.F.,.F.,(4,3,3,3,3,3,4),(-14.947051955369,
-14.5233980379778,-13.5551715021126,-12.5869449662474,-11.6187184303822,
-10.650491894517,-10.3764180272043),.UNSPECIFIED.);
#2827=B_SPLINE_CURVE_WITH_KNOTS('',3,(#43670,#43671,#43672,#43673,#43674,
#43675,#43676,#43677,#43678),.UNSPECIFIED.,.F.,.F.,(4,1,1,1,1,1,4),(10.3764180272043,
11.2351127702943,12.2101850432079,13.1852573161216,14.1603295890352,15.1354018619488,
15.707963267949),.UNSPECIFIED.);
#2828=B_SPLINE_CURVE_WITH_KNOTS('',3,(#43776,#43777,#43778,#43779,#43780,
#43781,#43782,#43783,#43784,#43785,#43786,#43787,#43788,#43789,#43790,#43791,
#43792,#43793,#43794,#43795,#43796,#43797),.UNSPECIFIED.,.F.,.F.,(4,3,3,
3,3,3,3,4),(7.39806731639555,7.80057818330904,8.77565045622267,9.7507227291363,
10.7257950020499,11.7008672749636,12.6759395478772,12.8805298797181),
 .UNSPECIFIED.);
#2829=B_SPLINE_CURVE_WITH_KNOTS('',3,(#43798,#43799,#43800,#43801,#43802,
#43803,#43804,#43805,#43806,#43807,#43808,#43809,#43810,#43811,#43812,#43813,
#43814,#43815,#43816,#43817,#43818,#43819,#43820,#43821,#43822,#43823,#43824,
#43825,#43826,#43827,#43828,#43829,#43830,#43831,#43832,#43833,#43834,#43835,
#43836,#43837,#43838,#43839,#43840,#43841,#43842,#43843,#43844,#43845,#43846,
#43847,#43848,#43849,#43850,#43851,#43852,#43853,#43854,#43855,#43856,#43857,
#43858,#43859,#43860,#43861),.UNSPECIFIED.,.F.,.F.,(4,3,3,3,3,3,3,3,3,3,
3,3,3,3,3,3,3,3,3,3,3,4),(-0.937740963081767,-0.889617493595049,-0.848304455696462,
-0.828682446370235,-0.760262135956028,-0.724356285684949,-0.705545676850033,
-0.633958254388594,-0.580112260350483,-0.555771314501388,-0.535484356147626,
-0.4642344184685,-0.40739310428294,-0.380133656928136,-0.358792074193013,
-0.284322152713594,-0.236869161726259,-0.198441507541726,-0.17634790638339,
-0.0995983283272545,-0.0229227240658628,0.),.UNSPECIFIED.);
#3438=LINE('',#43133,#4070);
#3439=LINE('',#43160,#4071);
#3440=LINE('',#43208,#4072);
#3441=LINE('',#43235,#4073);
#3442=LINE('',#43485,#4074);
#3443=LINE('',#43866,#4075);
#3444=LINE('',#43868,#4076);
#3445=LINE('',#43870,#4077);
#3446=LINE('',#43871,#4078);
#3447=LINE('',#43874,#4079);
#3448=LINE('',#43876,#4080);
#3449=LINE('',#43877,#4081);
#3450=LINE('',#43880,#4082);
#3451=LINE('',#43882,#4083);
#3452=LINE('',#43883,#4084);
#3453=LINE('',#43886,#4085);
#3454=LINE('',#43888,#4086);
#3455=LINE('',#43889,#4087);
#3456=LINE('',#43892,#4088);
#3457=LINE('',#43894,#4089);
#3458=LINE('',#43895,#4090);
#3459=LINE('',#43897,#4091);
#3460=LINE('',#43898,#4092);
#3461=LINE('',#43905,#4093);
#4070=VECTOR('',#14421,0.5);
#4071=VECTOR('',#14426,0.5);
#4072=VECTOR('',#14429,0.40705);
#4073=VECTOR('',#14434,0.40705);
#4074=VECTOR('',#14439,0.45);
#4075=VECTOR('',#14450,1.);
#4076=VECTOR('',#14451,1.);
#4077=VECTOR('',#14452,1.);
#4078=VECTOR('',#14453,1.);
#4079=VECTOR('',#14456,1.);
#4080=VECTOR('',#14457,1.);
#4081=VECTOR('',#14458,1.);
#4082=VECTOR('',#14461,1.);
#4083=VECTOR('',#14462,1.);
#4084=VECTOR('',#14463,1.);
#4085=VECTOR('',#14466,1.);
#4086=VECTOR('',#14467,1.);
#4087=VECTOR('',#14468,1.);
#4088=VECTOR('',#14471,1.);
#4089=VECTOR('',#14472,1.);
#4090=VECTOR('',#14473,1.);
#4091=VECTOR('',#14476,1.);
#4092=VECTOR('',#14477,1.);
#4093=VECTOR('',#14486,0.6);
#5168=VERTEX_POINT('',#43131);
#5169=VERTEX_POINT('',#43132);
#5170=VERTEX_POINT('',#43134);
#5171=VERTEX_POINT('',#43145);
#5172=VERTEX_POINT('',#43158);
#5173=VERTEX_POINT('',#43159);
#5174=VERTEX_POINT('',#43206);
#5175=VERTEX_POINT('',#43207);
#5176=VERTEX_POINT('',#43209);
#5177=VERTEX_POINT('',#43221);
#5178=VERTEX_POINT('',#43233);
#5179=VERTEX_POINT('',#43234);
#5180=VERTEX_POINT('',#43258);
#5181=VERTEX_POINT('',#43407);
#5182=VERTEX_POINT('',#43457);
#5183=VERTEX_POINT('',#43484);
#5184=VERTEX_POINT('',#43575);
#5185=VERTEX_POINT('',#43669);
#5186=VERTEX_POINT('',#43864);
#5187=VERTEX_POINT('',#43865);
#5188=VERTEX_POINT('',#43867);
#5189=VERTEX_POINT('',#43869);
#5190=VERTEX_POINT('',#43873);
#5191=VERTEX_POINT('',#43875);
#5192=VERTEX_POINT('',#43879);
#5193=VERTEX_POINT('',#43881);
#5194=VERTEX_POINT('',#43885);
#5195=VERTEX_POINT('',#43887);
#5196=VERTEX_POINT('',#43891);
#5197=VERTEX_POINT('',#43893);
#5198=VERTEX_POINT('',#43901);
#5199=VERTEX_POINT('',#43904);
#6813=EDGE_CURVE('',#5168,#5169,#3438,.T.);
#6814=EDGE_CURVE('',#5168,#5170,#2813,.T.);
#6815=EDGE_CURVE('',#5170,#5171,#1985,.F.);
#6816=EDGE_CURVE('',#5171,#5169,#2814,.T.);
#6817=EDGE_CURVE('',#5172,#5173,#3439,.T.);
#6818=EDGE_CURVE('',#5172,#5168,#2815,.T.);
#6819=EDGE_CURVE('',#5169,#5173,#2816,.T.);
#6820=EDGE_CURVE('',#5174,#5175,#3440,.T.);
#6821=EDGE_CURVE('',#5174,#5176,#2817,.T.);
#6822=EDGE_CURVE('',#5176,#5177,#1986,.T.);
#6823=EDGE_CURVE('',#5175,#5177,#2818,.T.);
#6824=EDGE_CURVE('',#5178,#5179,#3441,.T.);
#6825=EDGE_CURVE('',#5178,#5174,#2819,.T.);
#6826=EDGE_CURVE('',#5179,#5175,#2820,.T.);
#6827=EDGE_CURVE('',#5177,#5180,#2821,.T.);
#6828=EDGE_CURVE('',#5181,#5176,#2822,.T.);
#6829=EDGE_CURVE('',#5182,#5181,#1987,.T.);
#6830=EDGE_CURVE('',#5180,#5182,#2823,.T.);
#6831=EDGE_CURVE('',#5180,#5183,#3442,.T.);
#6832=EDGE_CURVE('',#5183,#5183,#1988,.T.);
#6833=EDGE_CURVE('',#5184,#5178,#2824,.T.);
#6834=EDGE_CURVE('',#5170,#5184,#2825,.T.);
#6835=EDGE_CURVE('',#5181,#5172,#2826,.T.);
#6836=EDGE_CURVE('',#5185,#5179,#2827,.T.);
#6837=EDGE_CURVE('',#5184,#5185,#1989,.T.);
#6838=EDGE_CURVE('',#5173,#5182,#2828,.T.);
#6839=EDGE_CURVE('',#5185,#5171,#2829,.T.);
#6840=EDGE_CURVE('',#5186,#5187,#3443,.T.);
#6841=EDGE_CURVE('',#5186,#5188,#3444,.T.);
#6842=EDGE_CURVE('',#5188,#5189,#3445,.T.);
#6843=EDGE_CURVE('',#5187,#5189,#3446,.T.);
#6844=EDGE_CURVE('',#5190,#5186,#3447,.T.);
#6845=EDGE_CURVE('',#5190,#5191,#3448,.T.);
#6846=EDGE_CURVE('',#5191,#5188,#3449,.T.);
#6847=EDGE_CURVE('',#5192,#5190,#3450,.T.);
#6848=EDGE_CURVE('',#5192,#5193,#3451,.T.);
#6849=EDGE_CURVE('',#5193,#5191,#3452,.T.);
#6850=EDGE_CURVE('',#5194,#5192,#3453,.T.);
#6851=EDGE_CURVE('',#5194,#5195,#3454,.T.);
#6852=EDGE_CURVE('',#5195,#5193,#3455,.T.);
#6853=EDGE_CURVE('',#5196,#5194,#3456,.T.);
#6854=EDGE_CURVE('',#5196,#5197,#3457,.T.);
#6855=EDGE_CURVE('',#5197,#5195,#3458,.T.);
#6856=EDGE_CURVE('',#5187,#5196,#3459,.T.);
#6857=EDGE_CURVE('',#5189,#5197,#3460,.T.);
#6858=EDGE_CURVE('',#5198,#5198,#1990,.T.);
#6859=EDGE_CURVE('',#5198,#5199,#3461,.T.);
#6860=EDGE_CURVE('',#5199,#5199,#1991,.T.);
#10087=ORIENTED_EDGE('',*,*,#6813,.F.);
#10088=ORIENTED_EDGE('',*,*,#6814,.T.);
#10089=ORIENTED_EDGE('',*,*,#6815,.T.);
#10090=ORIENTED_EDGE('',*,*,#6816,.T.);
#10091=ORIENTED_EDGE('',*,*,#6817,.F.);
#10092=ORIENTED_EDGE('',*,*,#6818,.T.);
#10093=ORIENTED_EDGE('',*,*,#6813,.T.);
#10094=ORIENTED_EDGE('',*,*,#6819,.T.);
#10095=ORIENTED_EDGE('',*,*,#6820,.F.);
#10096=ORIENTED_EDGE('',*,*,#6821,.T.);
#10097=ORIENTED_EDGE('',*,*,#6822,.T.);
#10098=ORIENTED_EDGE('',*,*,#6823,.F.);
#10099=ORIENTED_EDGE('',*,*,#6824,.F.);
#10100=ORIENTED_EDGE('',*,*,#6825,.T.);
#10101=ORIENTED_EDGE('',*,*,#6820,.T.);
#10102=ORIENTED_EDGE('',*,*,#6826,.F.);
#10103=ORIENTED_EDGE('',*,*,#6827,.F.);
#10104=ORIENTED_EDGE('',*,*,#6822,.F.);
#10105=ORIENTED_EDGE('',*,*,#6828,.F.);
#10106=ORIENTED_EDGE('',*,*,#6829,.F.);
#10107=ORIENTED_EDGE('',*,*,#6830,.F.);
#10108=ORIENTED_EDGE('',*,*,#6831,.T.);
#10109=ORIENTED_EDGE('',*,*,#6832,.F.);
#10110=ORIENTED_EDGE('',*,*,#6831,.F.);
#10111=ORIENTED_EDGE('',*,*,#6828,.T.);
#10112=ORIENTED_EDGE('',*,*,#6821,.F.);
#10113=ORIENTED_EDGE('',*,*,#6825,.F.);
#10114=ORIENTED_EDGE('',*,*,#6833,.F.);
#10115=ORIENTED_EDGE('',*,*,#6834,.F.);
#10116=ORIENTED_EDGE('',*,*,#6814,.F.);
#10117=ORIENTED_EDGE('',*,*,#6818,.F.);
#10118=ORIENTED_EDGE('',*,*,#6835,.F.);
#10119=ORIENTED_EDGE('',*,*,#6824,.T.);
#10120=ORIENTED_EDGE('',*,*,#6836,.F.);
#10121=ORIENTED_EDGE('',*,*,#6837,.F.);
#10122=ORIENTED_EDGE('',*,*,#6833,.T.);
#10123=ORIENTED_EDGE('',*,*,#6827,.T.);
#10124=ORIENTED_EDGE('',*,*,#6830,.T.);
#10125=ORIENTED_EDGE('',*,*,#6838,.F.);
#10126=ORIENTED_EDGE('',*,*,#6819,.F.);
#10127=ORIENTED_EDGE('',*,*,#6816,.F.);
#10128=ORIENTED_EDGE('',*,*,#6839,.F.);
#10129=ORIENTED_EDGE('',*,*,#6836,.T.);
#10130=ORIENTED_EDGE('',*,*,#6826,.T.);
#10131=ORIENTED_EDGE('',*,*,#6823,.T.);
#10132=ORIENTED_EDGE('',*,*,#6817,.T.);
#10133=ORIENTED_EDGE('',*,*,#6838,.T.);
#10134=ORIENTED_EDGE('',*,*,#6829,.T.);
#10135=ORIENTED_EDGE('',*,*,#6835,.T.);
#10136=ORIENTED_EDGE('',*,*,#6840,.F.);
#10137=ORIENTED_EDGE('',*,*,#6841,.T.);
#10138=ORIENTED_EDGE('',*,*,#6842,.T.);
#10139=ORIENTED_EDGE('',*,*,#6843,.F.);
#10140=ORIENTED_EDGE('',*,*,#6844,.F.);
#10141=ORIENTED_EDGE('',*,*,#6845,.T.);
#10142=ORIENTED_EDGE('',*,*,#6846,.T.);
#10143=ORIENTED_EDGE('',*,*,#6841,.F.);
#10144=ORIENTED_EDGE('',*,*,#6847,.F.);
#10145=ORIENTED_EDGE('',*,*,#6848,.T.);
#10146=ORIENTED_EDGE('',*,*,#6849,.T.);
#10147=ORIENTED_EDGE('',*,*,#6845,.F.);
#10148=ORIENTED_EDGE('',*,*,#6850,.F.);
#10149=ORIENTED_EDGE('',*,*,#6851,.T.);
#10150=ORIENTED_EDGE('',*,*,#6852,.T.);
#10151=ORIENTED_EDGE('',*,*,#6848,.F.);
#10152=ORIENTED_EDGE('',*,*,#6853,.F.);
#10153=ORIENTED_EDGE('',*,*,#6854,.T.);
#10154=ORIENTED_EDGE('',*,*,#6855,.T.);
#10155=ORIENTED_EDGE('',*,*,#6851,.F.);
#10156=ORIENTED_EDGE('',*,*,#6856,.F.);
#10157=ORIENTED_EDGE('',*,*,#6843,.T.);
#10158=ORIENTED_EDGE('',*,*,#6857,.T.);
#10159=ORIENTED_EDGE('',*,*,#6854,.F.);
#10160=ORIENTED_EDGE('',*,*,#6857,.F.);
#10161=ORIENTED_EDGE('',*,*,#6842,.F.);
#10162=ORIENTED_EDGE('',*,*,#6846,.F.);
#10163=ORIENTED_EDGE('',*,*,#6849,.F.);
#10164=ORIENTED_EDGE('',*,*,#6852,.F.);
#10165=ORIENTED_EDGE('',*,*,#6855,.F.);
#10166=ORIENTED_EDGE('',*,*,#6858,.T.);
#10167=ORIENTED_EDGE('',*,*,#6834,.T.);
#10168=ORIENTED_EDGE('',*,*,#6837,.T.);
#10169=ORIENTED_EDGE('',*,*,#6839,.T.);
#10170=ORIENTED_EDGE('',*,*,#6815,.F.);
#10171=ORIENTED_EDGE('',*,*,#6858,.F.);
#10172=ORIENTED_EDGE('',*,*,#6859,.T.);
#10173=ORIENTED_EDGE('',*,*,#6860,.T.);
#10174=ORIENTED_EDGE('',*,*,#6859,.F.);
#10175=ORIENTED_EDGE('',*,*,#6860,.F.);
#10176=ORIENTED_EDGE('',*,*,#6840,.T.);
#10177=ORIENTED_EDGE('',*,*,#6856,.T.);
#10178=ORIENTED_EDGE('',*,*,#6853,.T.);
#10179=ORIENTED_EDGE('',*,*,#6850,.T.);
#10180=ORIENTED_EDGE('',*,*,#6847,.T.);
#10181=ORIENTED_EDGE('',*,*,#6844,.T.);
#10182=ORIENTED_EDGE('',*,*,#6832,.T.);
#10602=CYLINDRICAL_SURFACE('',#12208,0.4925);
#10603=CYLINDRICAL_SURFACE('',#12210,0.4925);
#10604=CYLINDRICAL_SURFACE('',#12211,0.40705);
#10605=CYLINDRICAL_SURFACE('',#12213,0.40705);
#10606=CYLINDRICAL_SURFACE('',#12217,0.40705);
#10607=CYLINDRICAL_SURFACE('',#12219,0.4925);
#10608=CYLINDRICAL_SURFACE('',#12229,0.6);
#11211=ADVANCED_FACE('',(#1086),#10602,.T.);
#11212=ADVANCED_FACE('',(#1087),#10603,.T.);
#11213=ADVANCED_FACE('',(#1088),#10604,.T.);
#11214=ADVANCED_FACE('',(#1089),#10605,.T.);
#11215=ADVANCED_FACE('',(#1090),#150,.T.);
#11216=ADVANCED_FACE('',(#1091),#256,.F.);
#11217=ADVANCED_FACE('',(#1092),#10606,.T.);
#11218=ADVANCED_FACE('',(#1093),#257,.F.);
#11219=ADVANCED_FACE('',(#1094),#10607,.T.);
#11220=ADVANCED_FACE('',(#1095),#474,.F.);
#11221=ADVANCED_FACE('',(#1096),#475,.F.);
#11222=ADVANCED_FACE('',(#1097),#476,.F.);
#11223=ADVANCED_FACE('',(#1098),#477,.F.);
#11224=ADVANCED_FACE('',(#1099),#478,.F.);
#11225=ADVANCED_FACE('',(#1100),#479,.F.);
#11226=ADVANCED_FACE('',(#1101),#480,.F.);
#11227=ADVANCED_FACE('',(#1102,#329),#481,.T.);
#11228=ADVANCED_FACE('',(#1103),#10608,.T.);
#11229=ADVANCED_FACE('',(#1104,#330),#482,.F.);
#11230=ADVANCED_FACE('',(#1105),#483,.T.);
#11247=CLOSED_SHELL('',(#11211,#11212,#11213,#11214,#11215,#11216,#11217,
#11218,#11219,#11220,#11221,#11222,#11223,#11224,#11225,#11226,#11227,#11228,
#11229,#11230));
#12207=AXIS2_PLACEMENT_3D('',#43129,#14417,#14418);
#12208=AXIS2_PLACEMENT_3D('',#43130,#14419,#14420);
#12209=AXIS2_PLACEMENT_3D('',#43146,#14422,#14423);
#12210=AXIS2_PLACEMENT_3D('',#43157,#14424,#14425);
#12211=AXIS2_PLACEMENT_3D('',#43205,#14427,#14428);
#12212=AXIS2_PLACEMENT_3D('',#43222,#14430,#14431);
#12213=AXIS2_PLACEMENT_3D('',#43232,#14432,#14433);
#12214=AXIS2_PLACEMENT_3D('',#43257,#14435,#14436);
#12215=AXIS2_PLACEMENT_3D('',#43458,#14437,#14438);
#12216=AXIS2_PLACEMENT_3D('',#43486,#14440,#14441);
#12217=AXIS2_PLACEMENT_3D('',#43668,#14442,#14443);
#12218=AXIS2_PLACEMENT_3D('',#43679,#14444,#14445);
#12219=AXIS2_PLACEMENT_3D('',#43862,#14446,#14447);
#12220=AXIS2_PLACEMENT_3D('',#43863,#14448,#14449);
#12221=AXIS2_PLACEMENT_3D('',#43872,#14454,#14455);
#12222=AXIS2_PLACEMENT_3D('',#43878,#14459,#14460);
#12223=AXIS2_PLACEMENT_3D('',#43884,#14464,#14465);
#12224=AXIS2_PLACEMENT_3D('',#43890,#14469,#14470);
#12225=AXIS2_PLACEMENT_3D('',#43896,#14474,#14475);
#12226=AXIS2_PLACEMENT_3D('',#43899,#14478,#14479);
#12227=AXIS2_PLACEMENT_3D('',#43900,#14480,#14481);
#12228=AXIS2_PLACEMENT_3D('',#43902,#14482,#14483);
#12229=AXIS2_PLACEMENT_3D('',#43903,#14484,#14485);
#12230=AXIS2_PLACEMENT_3D('',#43906,#14487,#14488);
#12231=AXIS2_PLACEMENT_3D('',#43907,#14489,#14490);
#12232=AXIS2_PLACEMENT_3D('',#43908,#14491,#14492);
#14417=DIRECTION('axis',(0.,0.,1.));
#14418=DIRECTION('refdir',(1.,0.,0.));
#14419=DIRECTION('center_axis',(0.,0.,1.));
#14420=DIRECTION('ref_axis',(1.,0.,0.));
#14421=DIRECTION('',(0.,0.,-1.));
#14422=DIRECTION('center_axis',(0.,0.,-1.));
#14423=DIRECTION('ref_axis',(1.,0.,0.));
#14424=DIRECTION('center_axis',(0.,0.,1.));
#14425=DIRECTION('ref_axis',(1.,0.,0.));
#14426=DIRECTION('',(0.,0.,-1.));
#14427=DIRECTION('center_axis',(0.,0.,1.));
#14428=DIRECTION('ref_axis',(0.995010084519338,-0.0997744040564514,0.));
#14429=DIRECTION('',(0.,0.,1.));
#14430=DIRECTION('center_axis',(0.,0.,-1.));
#14431=DIRECTION('ref_axis',(1.,2.96346172991068E-16,0.));
#14432=DIRECTION('center_axis',(0.,0.,1.));
#14433=DIRECTION('ref_axis',(1.,2.96346172991068E-16,0.));
#14434=DIRECTION('',(0.,0.,1.));
#14435=DIRECTION('center_axis',(0.,0.,-1.));
#14436=DIRECTION('ref_axis',(1.,0.,0.));
#14437=DIRECTION('center_axis',(0.,0.,-1.));
#14438=DIRECTION('ref_axis',(1.,0.,0.));
#14439=DIRECTION('',(0.707106781186547,8.65956056235493E-17,0.707106781186548));
#14440=DIRECTION('center_axis',(0.,0.,1.));
#14441=DIRECTION('ref_axis',(1.,0.,0.));
#14442=DIRECTION('center_axis',(0.,0.,1.));
#14443=DIRECTION('ref_axis',(0.889042129798311,0.457825394057258,0.));
#14444=DIRECTION('center_axis',(0.,0.,-1.));
#14445=DIRECTION('ref_axis',(1.,2.96346172991068E-16,0.));
#14446=DIRECTION('center_axis',(0.,0.,1.));
#14447=DIRECTION('ref_axis',(1.,0.,0.));
#14448=DIRECTION('center_axis',(-1.92296268638356E-16,-1.,0.));
#14449=DIRECTION('ref_axis',(1.,-1.92296268638356E-16,0.));
#14450=DIRECTION('',(1.,-1.92296268638356E-16,0.));
#14451=DIRECTION('',(0.,0.,1.));
#14452=DIRECTION('',(1.,-1.92296268638356E-16,0.));
#14453=DIRECTION('',(0.,0.,1.));
#14454=DIRECTION('center_axis',(-0.866025403784439,-0.5,0.));
#14455=DIRECTION('ref_axis',(0.5,-0.866025403784439,0.));
#14456=DIRECTION('',(0.5,-0.866025403784439,0.));
#14457=DIRECTION('',(0.,0.,1.));
#14458=DIRECTION('',(0.5,-0.866025403784439,0.));
#14459=DIRECTION('center_axis',(-0.866025403784439,0.5,0.));
#14460=DIRECTION('ref_axis',(-0.5,-0.866025403784439,0.));
#14461=DIRECTION('',(-0.5,-0.866025403784439,0.));
#14462=DIRECTION('',(0.,0.,1.));
#14463=DIRECTION('',(-0.5,-0.866025403784438,0.));
#14464=DIRECTION('center_axis',(1.92296268638356E-16,1.,0.));
#14465=DIRECTION('ref_axis',(-1.,1.92296268638356E-16,0.));
#14466=DIRECTION('',(-1.,1.92296268638356E-16,0.));
#14467=DIRECTION('',(0.,0.,1.));
#14468=DIRECTION('',(-1.,1.92296268638356E-16,0.));
#14469=DIRECTION('center_axis',(0.866025403784439,0.5,0.));
#14470=DIRECTION('ref_axis',(-0.5,0.866025403784439,0.));
#14471=DIRECTION('',(-0.5,0.866025403784439,0.));
#14472=DIRECTION('',(0.,0.,1.));
#14473=DIRECTION('',(-0.5,0.866025403784439,0.));
#14474=DIRECTION('center_axis',(0.866025403784439,-0.5,0.));
#14475=DIRECTION('ref_axis',(0.5,0.866025403784439,0.));
#14476=DIRECTION('',(0.5,0.866025403784439,0.));
#14477=DIRECTION('',(0.5,0.866025403784439,0.));
#14478=DIRECTION('center_axis',(0.,0.,1.));
#14479=DIRECTION('ref_axis',(1.,0.,0.));
#14480=DIRECTION('center_axis',(0.,0.,1.));
#14481=DIRECTION('ref_axis',(1.,0.,0.));
#14482=DIRECTION('center_axis',(0.,0.,1.));
#14483=DIRECTION('ref_axis',(1.,0.,0.));
#14484=DIRECTION('center_axis',(0.,0.,1.));
#14485=DIRECTION('ref_axis',(1.,0.,0.));
#14486=DIRECTION('',(0.,0.,-1.));
#14487=DIRECTION('center_axis',(0.,0.,1.));
#14488=DIRECTION('ref_axis',(1.,0.,0.));
#14489=DIRECTION('center_axis',(0.,0.,1.));
#14490=DIRECTION('ref_axis',(1.,0.,0.));
#14491=DIRECTION('center_axis',(0.,0.,1.));
#14492=DIRECTION('ref_axis',(1.,0.,0.));
#43129=CARTESIAN_POINT('',(0.,0.,0.));
#43130=CARTESIAN_POINT('Origin',(0.,0.,0.));
#43131=CARTESIAN_POINT('',(-0.492481417404046,0.000356103300314048,0.0483841525903583));
#43132=CARTESIAN_POINT('',(-0.492579697791124,0.00014242512799704,0.0266158474096417));
#43133=CARTESIAN_POINT('',(-0.4925,-6.03138548580071E-17,0.));
#43134=CARTESIAN_POINT('',(0.216839587231055,0.442195480991683,0.));
#43135=CARTESIAN_POINT('Ctrl Pts',(-0.492481417404046,0.000356103300314048,
0.0483841525903583));
#43136=CARTESIAN_POINT('Ctrl Pts',(-0.492781970042288,0.0365118891852549,
0.0466308494026249));
#43137=CARTESIAN_POINT('Ctrl Pts',(-0.489117551943374,0.0726092955132097,
0.0448775462148916));
#43138=CARTESIAN_POINT('Ctrl Pts',(-0.481251921643029,0.107767962452072,
0.0431242430271582));
#43139=CARTESIAN_POINT('Ctrl Pts',(-0.446686359481315,0.262272946947089,
0.0354193410663739));
#43140=CARTESIAN_POINT('Ctrl Pts',(-0.330988306870102,0.398649291214372,
0.0277144391055896));
#43141=CARTESIAN_POINT('Ctrl Pts',(-0.184035775927903,0.457657279283401,
0.0200095371448053));
#43142=CARTESIAN_POINT('Ctrl Pts',(-0.0568244611321571,0.508738289576891,
0.0133396914298702));
#43143=CARTESIAN_POINT('Ctrl Pts',(0.0938080781422166,0.501841636033798,
0.00666984571493511));
#43144=CARTESIAN_POINT('Ctrl Pts',(0.217447815076511,0.442338803773993,
3.90312782094782E-18));
#43145=CARTESIAN_POINT('',(-0.216839587231055,0.442195480991683,0.));
#43146=CARTESIAN_POINT('Origin',(0.,0.,0.));
#43147=CARTESIAN_POINT('Ctrl Pts',(-0.216839587231054,0.442195480991683,
0.));
#43148=CARTESIAN_POINT('Ctrl Pts',(-0.288701679351503,0.406956436128511,
0.00387968930265135));
#43149=CARTESIAN_POINT('Ctrl Pts',(-0.351338791070612,0.353873869634597,
0.00775937860530267));
#43150=CARTESIAN_POINT('Ctrl Pts',(-0.398480091786207,0.289102201512631,
0.011639067907954));
#43151=CARTESIAN_POINT('Ctrl Pts',(-0.445621392501803,0.224330533390666,
0.0155187572106054));
#43152=CARTESIAN_POINT('Ctrl Pts',(-0.477266882213885,0.147869763640648,
0.0193984465132567));
#43153=CARTESIAN_POINT('Ctrl Pts',(-0.488203763978274,0.068702451394776,
0.0232781358159081));
#43154=CARTESIAN_POINT('Ctrl Pts',(-0.491340111094124,0.0459998038960704,
0.0243907063471526));
#43155=CARTESIAN_POINT('Ctrl Pts',(-0.492773468136237,0.0230745815620001,
0.0255032768783972));
#43156=CARTESIAN_POINT('Ctrl Pts',(-0.492579697791124,0.00014242512799704,
0.0266158474096417));
#43157=CARTESIAN_POINT('Origin',(0.,0.,0.));
#43158=CARTESIAN_POINT('',(-0.492300964172325,-0.000364928074014725,0.198384152590358));
#43159=CARTESIAN_POINT('',(-0.491861190935719,-0.000202060802622812,0.176615847409642));
#43160=CARTESIAN_POINT('',(-0.4925,-6.03138548580071E-17,0.));
#43161=CARTESIAN_POINT('Ctrl Pts',(-0.492300964172325,-0.000364928074014725,
0.198384152590358));
#43162=CARTESIAN_POINT('Ctrl Pts',(-0.491417602280064,0.113686713783483,
0.192860261167331));
#43163=CARTESIAN_POINT('Ctrl Pts',(-0.451685363551956,0.228287340070974,
0.187336369744303));
#43164=CARTESIAN_POINT('Ctrl Pts',(-0.379073885019767,0.315519852460857,
0.181812478321276));
#43165=CARTESIAN_POINT('Ctrl Pts',(-0.2777930522746,0.43719457491378,0.174107576360492));
#43166=CARTESIAN_POINT('Ctrl Pts',(-0.11254378321799,0.505623070834234,
0.166402674399707));
#43167=CARTESIAN_POINT('Ctrl Pts',(0.0451027730094741,0.491145507720989,
0.158697772438923));
#43168=CARTESIAN_POINT('Ctrl Pts',(0.202749329236939,0.476667944607744,
0.150992870478139));
#43169=CARTESIAN_POINT('Ctrl Pts',(0.352793172635258,0.379284322460801,
0.143287968517354));
#43170=CARTESIAN_POINT('Ctrl Pts',(0.430212224753047,0.241196209673131,
0.13558306655657));
#43171=CARTESIAN_POINT('Ctrl Pts',(0.507631276870837,0.103108096885462,
0.127878164595786));
#43172=CARTESIAN_POINT('Ctrl Pts',(0.512425537708097,-0.0756845065429327,
0.120173262635001));
#43173=CARTESIAN_POINT('Ctrl Pts',(0.442539342879764,-0.217735430292011,
0.112468360674217));
#43174=CARTESIAN_POINT('Ctrl Pts',(0.372653148051431,-0.35978635404109,
0.104763458713433));
#43175=CARTESIAN_POINT('Ctrl Pts',(0.228086497557505,-0.465095598110853,
0.0970585567526484));
#43176=CARTESIAN_POINT('Ctrl Pts',(0.0714359265950831,-0.488016791697039,
0.0893536547918641));
#43177=CARTESIAN_POINT('Ctrl Pts',(-0.0852146443673392,-0.510937985283226,
0.0816487528310798));
#43178=CARTESIAN_POINT('Ctrl Pts',(-0.253949135798258,-0.451471128385836,
0.0739438508702954));
#43179=CARTESIAN_POINT('Ctrl Pts',(-0.361599845657609,-0.335420887575765,
0.0662389489095111));
#43180=CARTESIAN_POINT('Ctrl Pts',(-0.444753899528498,-0.245778673523871,
0.0602873501364602));
#43181=CARTESIAN_POINT('Ctrl Pts',(-0.491461189570368,-0.122374940832272,
0.0543357513634092));
#43182=CARTESIAN_POINT('Ctrl Pts',(-0.492481417404046,0.000356103300314048,
0.0483841525903583));
#43183=CARTESIAN_POINT('Ctrl Pts',(-0.492579697791124,0.00014242512799704,
0.0266158474096417));
#43184=CARTESIAN_POINT('Ctrl Pts',(-0.491422059458777,-0.136860702548402,
0.0332626554836999));
#43185=CARTESIAN_POINT('Ctrl Pts',(-0.43218895190202,-0.274111322283754,
0.039909463557758));
#43186=CARTESIAN_POINT('Ctrl Pts',(-0.331056890567679,-0.365627465232998,
0.0465562716318162));
#43187=CARTESIAN_POINT('Ctrl Pts',(-0.212996921890301,-0.472461962893863,
0.0543156502371188));
#43188=CARTESIAN_POINT('Ctrl Pts',(-0.0378376527975418,-0.516970163740431,
0.0620750288424216));
#43189=CARTESIAN_POINT('Ctrl Pts',(0.117082871749507,-0.479203433651414,
0.0698344074477242));
#43190=CARTESIAN_POINT('Ctrl Pts',(0.272003396296556,-0.441436703562397,
0.077593786053027));
#43191=CARTESIAN_POINT('Ctrl Pts',(0.406685176297894,-0.321395042537794,
0.0853531646583296));
#43192=CARTESIAN_POINT('Ctrl Pts',(0.46224191715632,-0.171962621091513,
0.0931125432636324));
#43193=CARTESIAN_POINT('Ctrl Pts',(0.517798658014746,-0.0225301996452326,
0.100871921868935));
#43194=CARTESIAN_POINT('Ctrl Pts',(0.494230359730261,0.156292982222727,
0.108631300474238));
#43195=CARTESIAN_POINT('Ctrl Pts',(0.401766762010813,0.286123680734623,
0.11639067907954));
#43196=CARTESIAN_POINT('Ctrl Pts',(0.309303164291365,0.415954379246519,
0.124150057684843));
#43197=CARTESIAN_POINT('Ctrl Pts',(0.147944267136953,0.496792594402351,
0.131909436290146));
#43198=CARTESIAN_POINT('Ctrl Pts',(-0.0114321433727825,0.493107659430119,
0.139668814895449));
#43199=CARTESIAN_POINT('Ctrl Pts',(-0.170808553882518,0.489422724457888,
0.147428193500751));
#43200=CARTESIAN_POINT('Ctrl Pts',(-0.328202477747577,0.401214639357593,
0.155187572106054));
#43201=CARTESIAN_POINT('Ctrl Pts',(-0.414565342728602,0.267223128123415,
0.162946950711357));
#43202=CARTESIAN_POINT('Ctrl Pts',(-0.465277525582474,0.188543454631027,
0.167503249610785));
#43203=CARTESIAN_POINT('Ctrl Pts',(-0.491498014918926,0.094077536942573,
0.172059548510213));
#43204=CARTESIAN_POINT('Ctrl Pts',(-0.491861190935719,-0.000202060802622812,
0.176615847409642));
#43205=CARTESIAN_POINT('Origin',(0.,0.,-0.277281266907388));
#43206=CARTESIAN_POINT('',(-0.406885497393593,-0.000301612126959839,0.247718733092612));
#43207=CARTESIAN_POINT('',(-0.407643323035318,5.2650356487962E-5,0.277281266907388));
#43208=CARTESIAN_POINT('',(-0.40705,-1.70476957675307E-16,-0.277281266907388));
#43209=CARTESIAN_POINT('',(-0.398956125446125,0.0807695020971151,0.39295));
#43210=CARTESIAN_POINT('Ctrl Pts',(-0.406885497393594,-0.00030161212695989,
0.247718733092612));
#43211=CARTESIAN_POINT('Ctrl Pts',(-0.407173762990612,-0.0375198404872463,
0.249899743630369));
#43212=CARTESIAN_POINT('Ctrl Pts',(-0.385791970676486,-0.205899073274862,
0.25978565612891));
#43213=CARTESIAN_POINT('Ctrl Pts',(-0.153651115557833,-0.451003868944285,
0.277376470588235));
#43214=CARTESIAN_POINT('Ctrl Pts',(0.284312994089833,-0.382152940416395,
0.300491176470589));
#43215=CARTESIAN_POINT('Ctrl Pts',(0.476331647790245,0.0175545413646465,
0.323605882352941));
#43216=CARTESIAN_POINT('Ctrl Pts',(0.254819026846725,0.402583723993036,
0.346720588235294));
#43217=CARTESIAN_POINT('Ctrl Pts',(-0.112351263190869,0.431821186557985,
0.365982843137255));
#43218=CARTESIAN_POINT('Ctrl Pts',(-0.327918115217093,0.266750651701983,
0.381392647058824));
#43219=CARTESIAN_POINT('Ctrl Pts',(-0.385922262909618,0.145149486647597,
0.389097549019608));
#43220=CARTESIAN_POINT('Ctrl Pts',(-0.398956125446125,0.0807695020971137,
0.39295));
#43221=CARTESIAN_POINT('',(-0.0538698874795526,0.403469624287802,0.39295));
#43222=CARTESIAN_POINT('Origin',(0.,0.,0.39295));
#43223=CARTESIAN_POINT('Ctrl Pts',(-0.407643323035318,5.26503564879819E-5,
0.277281266907388));
#43224=CARTESIAN_POINT('Ctrl Pts',(-0.407328549577932,-0.127609068365495,
0.284799996850381));
#43225=CARTESIAN_POINT('Ctrl Pts',(-0.275150626354469,-0.387484704349645,
0.300078105398677));
#43226=CARTESIAN_POINT('Ctrl Pts',(0.163268921903001,-0.448972926511222,
0.323115592552276));
#43227=CARTESIAN_POINT('Ctrl Pts',(0.463203848138002,-0.116047052095292,
0.346393728368184));
#43228=CARTESIAN_POINT('Ctrl Pts',(0.373893623429547,0.244589772389548,
0.365792174881441));
#43229=CARTESIAN_POINT('Ctrl Pts',(0.146530577079214,0.396735441137677,
0.381310932092046));
#43230=CARTESIAN_POINT('Ctrl Pts',(0.0116987864547665,0.412224129892184,
0.389070310697349));
#43231=CARTESIAN_POINT('Ctrl Pts',(-0.0538698874795526,0.403469624287802,
0.39295));
#43232=CARTESIAN_POINT('Origin',(0.,0.,-0.277281266907388));
#43233=CARTESIAN_POINT('',(-0.407034641531608,0.00029431847389476,0.0977187330926118));
#43234=CARTESIAN_POINT('',(-0.406522025929715,-0.00016700274052156,0.127281266907388));
#43235=CARTESIAN_POINT('',(-0.40705,-1.70476957675307E-16,-0.277281266907388));
#43236=CARTESIAN_POINT('Ctrl Pts',(-0.407034641531608,0.000294318473894748,
0.0977187330926118));
#43237=CARTESIAN_POINT('Ctrl Pts',(-0.406191425816484,-0.101142578001576,
0.103670331865663));
#43238=CARTESIAN_POINT('Ctrl Pts',(-0.317612179383904,-0.335174773810633,
0.117326832599498));
#43239=CARTESIAN_POINT('Ctrl Pts',(0.0690289416187412,-0.471438154334252,
0.138688235294118));
#43240=CARTESIAN_POINT('Ctrl Pts',(0.427480850757132,-0.210324685510313,
0.161802941176471));
#43241=CARTESIAN_POINT('Ctrl Pts',(0.41559351751567,0.232990213325393,0.184917647058823));
#43242=CARTESIAN_POINT('Ctrl Pts',(0.0435609502753498,0.474452162939076,
0.208032352941177));
#43243=CARTESIAN_POINT('Ctrl Pts',(-0.32751247561348,0.320793411196436,
0.228966048285772));
#43244=CARTESIAN_POINT('Ctrl Pts',(-0.406155401031675,0.09396178039709,
0.242194841669584));
#43245=CARTESIAN_POINT('Ctrl Pts',(-0.406885497393594,-0.00030161212695989,
0.247718733092612));
#43246=CARTESIAN_POINT('Ctrl Pts',(-0.406522025929715,-0.000167002740521567,
0.127281266907388));
#43247=CARTESIAN_POINT('Ctrl Pts',(-0.406733041365224,-0.0549460890728457,
0.130484346613262));
#43248=CARTESIAN_POINT('Ctrl Pts',(-0.371307907491832,-0.242165643317298,
0.141446804924439));
#43249=CARTESIAN_POINT('Ctrl Pts',(-0.0916847062669661,-0.468629856473293,
0.160168641840919));
#43250=CARTESIAN_POINT('Ctrl Pts',(0.336453410254844,-0.338849716643417,
0.183446777656827));
#43251=CARTESIAN_POINT('Ctrl Pts',(0.46926975494663,0.088378354603048,0.206724913472736));
#43252=CARTESIAN_POINT('Ctrl Pts',(0.190156376929569,0.437998801366229,
0.230003049288643));
#43253=CARTESIAN_POINT('Ctrl Pts',(-0.255854007963939,0.403215004461254,
0.253281185104552));
#43254=CARTESIAN_POINT('Ctrl Pts',(-0.405783805870032,0.139964592457054,
0.269040590977466));
#43255=CARTESIAN_POINT('Ctrl Pts',(-0.407653397850083,0.0041386624983676,
0.277040618245079));
#43256=CARTESIAN_POINT('Ctrl Pts',(-0.407643323035318,5.26503564879819E-5,
0.277281266907388));
#43257=CARTESIAN_POINT('Origin',(0.,0.,0.35));
#43258=CARTESIAN_POINT('',(-0.481004250423532,5.53027357347368E-5,0.319618961639866));
#43259=CARTESIAN_POINT('Ctrl Pts',(-0.0538698874795498,0.403469624287803,
0.39295));
#43260=CARTESIAN_POINT('Ctrl Pts',(-0.0316653326884239,0.407278826215671,
0.392112902831245));
#43261=CARTESIAN_POINT('Ctrl Pts',(-0.00924491338711062,0.409176650041635,
0.391280875609609));
#43262=CARTESIAN_POINT('Ctrl Pts',(0.0131866458412135,0.409236810812678,
0.390451027642853));
#43263=CARTESIAN_POINT('Ctrl Pts',(0.0268208116764566,0.409273377237724,
0.389946636277027));
#43264=CARTESIAN_POINT('Ctrl Pts',(0.040459458237955,0.408630029143461,
0.389443050004563));
#43265=CARTESIAN_POINT('Ctrl Pts',(0.0540577419912376,0.407314101233933,
0.388939619729085));
#43266=CARTESIAN_POINT('Ctrl Pts',(0.0622889918244366,0.406517549876253,
0.388634885657769));
#43267=CARTESIAN_POINT('Ctrl Pts',(0.0705093035012178,0.405473504159666,
0.388330064318474));
#43268=CARTESIAN_POINT('Ctrl Pts',(0.0786814053095045,0.404187608479032,
0.388026026559159));
#43269=CARTESIAN_POINT('Ctrl Pts',(0.100768052332083,0.40071223278349,0.38720430714975));
#43270=CARTESIAN_POINT('Ctrl Pts',(0.122540335589337,0.395471779259362,
0.386386924436749));
#43271=CARTESIAN_POINT('Ctrl Pts',(0.143803418736277,0.388506736509305,
0.38557112662273));
#43272=CARTESIAN_POINT('Ctrl Pts',(0.156170109258924,0.384455840993744,
0.3850966554924));
#43273=CARTESIAN_POINT('Ctrl Pts',(0.168364571979357,0.379820676364071,
0.384622720474772));
#43274=CARTESIAN_POINT('Ctrl Pts',(0.180342700215435,0.374619772055251,
0.38414878019481));
#43275=CARTESIAN_POINT('Ctrl Pts',(0.186280745973306,0.372041472077208,
0.383913828705442));
#43276=CARTESIAN_POINT('Ctrl Pts',(0.192158160674688,0.369327168271282,
0.38367916801279));
#43277=CARTESIAN_POINT('Ctrl Pts',(0.197963597616422,0.366483083438636,
0.38344498715594));
#43278=CARTESIAN_POINT('Ctrl Pts',(0.219836146361836,0.355767717004984,
0.382562687983959));
#43279=CARTESIAN_POINT('Ctrl Pts',(0.240716970738482,0.343202582426593,
0.381686072170868));
#43280=CARTESIAN_POINT('Ctrl Pts',(0.260332898611107,0.328932743376239,
0.380811747318508));
#43281=CARTESIAN_POINT('Ctrl Pts',(0.278594803461462,0.315647904409681,
0.379997774236746));
#43282=CARTESIAN_POINT('Ctrl Pts',(0.295761578458153,0.300884440199882,
0.379185786756448));
#43283=CARTESIAN_POINT('Ctrl Pts',(0.311586138874096,0.284716704150859,
0.378373047602317));
#43284=CARTESIAN_POINT('Ctrl Pts',(0.312759445782441,0.283517952596312,
0.378312787320883));
#43285=CARTESIAN_POINT('Ctrl Pts',(0.313925356487753,0.282311464687701,
0.378252522907174));
#43286=CARTESIAN_POINT('Ctrl Pts',(0.315083761312798,0.281097263038206,
0.378192253245459));
#43287=CARTESIAN_POINT('Ctrl Pts',(0.318831185432892,0.27716933693707,0.377997281695672));
#43288=CARTESIAN_POINT('Ctrl Pts',(0.322493195092308,0.273167891631071,
0.377802612506538));
#43289=CARTESIAN_POINT('Ctrl Pts',(0.326069508835965,0.269096914837346,
0.377608226014736));
#43290=CARTESIAN_POINT('Ctrl Pts',(0.341206374273448,0.251866371785855,
0.376785478800656));
#43291=CARTESIAN_POINT('Ctrl Pts',(0.354812779827501,0.233391506862419,
0.375967697324452));
#43292=CARTESIAN_POINT('Ctrl Pts',(0.366870039940409,0.213921252206375,
0.375152133928824));
#43293=CARTESIAN_POINT('Ctrl Pts',(0.376130504932898,0.198967306621001,
0.374525748149332));
#43294=CARTESIAN_POINT('Ctrl Pts',(0.384476533461525,0.183425031595393,
0.373900670785239));
#43295=CARTESIAN_POINT('Ctrl Pts',(0.391884013928886,0.167394361930957,
0.373275656992184));
#43296=CARTESIAN_POINT('Ctrl Pts',(0.395222611144067,0.160169240064625,
0.372993959413886));
#43297=CARTESIAN_POINT('Ctrl Pts',(0.398370359701117,0.152844794166232,
0.372712274749158));
#43298=CARTESIAN_POINT('Ctrl Pts',(0.401324042121161,0.145429744486488,
0.372430489026677));
#43299=CARTESIAN_POINT('Ctrl Pts',(0.403162482847082,0.140814444878291,
0.372255099030556));
#43300=CARTESIAN_POINT('Ctrl Pts',(0.404925063262203,0.136165420236397,
0.37207972382087));
#43301=CARTESIAN_POINT('Ctrl Pts',(0.406608059344916,0.131493954632065,
0.371904674370206));
#43302=CARTESIAN_POINT('Ctrl Pts',(0.414696192879373,0.10904385032253,0.371063422660446));
#43303=CARTESIAN_POINT('Ctrl Pts',(0.420972938099192,0.0860210152190577,
0.370227536000813));
#43304=CARTESIAN_POINT('Ctrl Pts',(0.425395909977663,0.0626759796342939,
0.369394086287783));
#43305=CARTESIAN_POINT('Ctrl Pts',(0.429018549770037,0.0435552035616685,
0.368711448419326));
#43306=CARTESIAN_POINT('Ctrl Pts',(0.431396924655892,0.0242172462070704,
0.368030445363422));
#43307=CARTESIAN_POINT('Ctrl Pts',(0.432482965195409,0.00479181875932576,
0.367349468256));
#43308=CARTESIAN_POINT('Ctrl Pts',(0.432895970962219,-0.00259539494657891,
0.367090502349851));
#43309=CARTESIAN_POINT('Ctrl Pts',(0.433121836997117,-0.00999528408518393,
0.3668315401963));
#43310=CARTESIAN_POINT('Ctrl Pts',(0.433156980509427,-0.0174007138892953,
0.366572493314436));
#43311=CARTESIAN_POINT('Ctrl Pts',(0.433183158031874,-0.0229168331438603,
0.366379535777779));
#43312=CARTESIAN_POINT('Ctrl Pts',(0.433103335387378,-0.0284349632594622,
0.366186568266144));
#43313=CARTESIAN_POINT('Ctrl Pts',(0.432916876988951,-0.0339394879965735,
0.36599399665361));
#43314=CARTESIAN_POINT('Ctrl Pts',(0.43208645521872,-0.0584547536806542,
0.365136348723961));
#43315=CARTESIAN_POINT('Ctrl Pts',(0.429146442859694,-0.0827663174634086,
0.36428421955312));
#43316=CARTESIAN_POINT('Ctrl Pts',(0.424019958835254,-0.106615431423388,
0.363434506490917));
#43317=CARTESIAN_POINT('Ctrl Pts',(0.420254969930063,-0.12413068145243,
0.362810460802579));
#43318=CARTESIAN_POINT('Ctrl Pts',(0.415309486405733,-0.141396959340888,
0.362187718294952));
#43319=CARTESIAN_POINT('Ctrl Pts',(0.409263192987451,-0.158338140935025,
0.361565049930666));
#43320=CARTESIAN_POINT('Ctrl Pts',(0.406160149386259,-0.167032595786217,
0.361245487688182));
#43321=CARTESIAN_POINT('Ctrl Pts',(0.402766875155836,-0.175641358171848,
0.360925944974225));
#43322=CARTESIAN_POINT('Ctrl Pts',(0.399092466924463,-0.184153510043428,
0.360606255653821));
#43323=CARTESIAN_POINT('Ctrl Pts',(0.396937681309731,-0.189145296815156,
0.360418780037228));
#43324=CARTESIAN_POINT('Ctrl Pts',(0.394687827641809,-0.194099817084966,
0.36023140397824));
#43325=CARTESIAN_POINT('Ctrl Pts',(0.392348729830297,-0.199007875093207,
0.360044367857094));
#43326=CARTESIAN_POINT('Ctrl Pts',(0.382074069665097,-0.220566882954087,
0.359222797859493));
#43327=CARTESIAN_POINT('Ctrl Pts',(0.370063481928657,-0.241272797950768,
0.358406199055954));
#43328=CARTESIAN_POINT('Ctrl Pts',(0.356513827665842,-0.260956061324833,
0.357591842535157));
#43329=CARTESIAN_POINT('Ctrl Pts',(0.344051171209901,-0.279060268606045,
0.356842816371501));
#43330=CARTESIAN_POINT('Ctrl Pts',(0.33028533438652,-0.29629992463707,0.35609568715483));
#43331=CARTESIAN_POINT('Ctrl Pts',(0.315336322124332,-0.312526310576975,
0.355348331461484));
#43332=CARTESIAN_POINT('Ctrl Pts',(0.310609992907685,-0.317656498485265,
0.355112045010799));
#43333=CARTESIAN_POINT('Ctrl Pts',(0.30576519313948,-0.322685232420505,
0.354875735921677));
#43334=CARTESIAN_POINT('Ctrl Pts',(0.300805202572924,-0.327607284714727,
0.354639337086618));
#43335=CARTESIAN_POINT('Ctrl Pts',(0.296833059963398,-0.331549044962422,
0.354450020217366));
#43336=CARTESIAN_POINT('Ctrl Pts',(0.292793666699487,-0.335415776601772,
0.354260962157573));
#43337=CARTESIAN_POINT('Ctrl Pts',(0.288690374812154,-0.339204472629103,
0.354072175529782));
#43338=CARTESIAN_POINT('Ctrl Pts',(0.270614704216604,-0.355894297105914,
0.353240539616353));
#43339=CARTESIAN_POINT('Ctrl Pts',(0.251296156517944,-0.371078438036047,
0.352413878354462));
#43340=CARTESIAN_POINT('Ctrl Pts',(0.230912254648246,-0.38456380919539,
0.351589358773348));
#43341=CARTESIAN_POINT('Ctrl Pts',(0.218893580948008,-0.392514999145518,
0.351103208875834));
#43342=CARTESIAN_POINT('Ctrl Pts',(0.206503719012034,-0.399875069206143,
0.350617803527155));
#43343=CARTESIAN_POINT('Ctrl Pts',(0.193773466861638,-0.406597848773312,
0.350132562030064));
#43344=CARTESIAN_POINT('Ctrl Pts',(0.185999255133483,-0.41070336931913,
0.349836230889636));
#43345=CARTESIAN_POINT('Ctrl Pts',(0.178098026299929,-0.414571112773857,
0.349539960855983));
#43346=CARTESIAN_POINT('Ctrl Pts',(0.170076244645801,-0.418189396436464,
0.349243619675404));
#43347=CARTESIAN_POINT('Ctrl Pts',(0.164962379018466,-0.420496043170314,
0.349054702918171));
#43348=CARTESIAN_POINT('Ctrl Pts',(0.159797829707925,-0.422701963634567,
0.348865696264321));
#43349=CARTESIAN_POINT('Ctrl Pts',(0.154589564749718,-0.424801769371719,
0.348676759736376));
#43350=CARTESIAN_POINT('Ctrl Pts',(0.132490547639595,-0.433711385776723,
0.347875089391783));
#43351=CARTESIAN_POINT('Ctrl Pts',(0.109712996458169,-0.440673017272614,
0.347078510447043));
#43352=CARTESIAN_POINT('Ctrl Pts',(0.0865025359672138,-0.445776648784633,
0.346284504867115));
#43353=CARTESIAN_POINT('Ctrl Pts',(0.0656695337547962,-0.450357512943821,
0.345571829648553));
#43354=CARTESIAN_POINT('Ctrl Pts',(0.044486654916784,-0.453440828959329,
0.344861227612633));
#43355=CARTESIAN_POINT('Ctrl Pts',(0.0231186212993554,-0.455059571778107,
0.344150877943281));
#43356=CARTESIAN_POINT('Ctrl Pts',(0.0130564925833783,-0.45582183183873,
0.343816376887435));
#43357=CARTESIAN_POINT('Ctrl Pts',(0.00295320522441201,-0.456258902299385,
0.343481931792199));
#43358=CARTESIAN_POINT('Ctrl Pts',(-0.00717423696244157,-0.456371949816793,
0.343147352531355));
#43359=CARTESIAN_POINT('Ctrl Pts',(-0.0143387859440224,-0.456451924055182,
0.342910658067115));
#43360=CARTESIAN_POINT('Ctrl Pts',(-0.0215180448808933,-0.456369369939335,
0.342673810145585));
#43361=CARTESIAN_POINT('Ctrl Pts',(-0.0286817505223104,-0.456125823134922,
0.342437538775626));
#43362=CARTESIAN_POINT('Ctrl Pts',(-0.0537451739868064,-0.455273733867443,
0.341610903833569));
#43363=CARTESIAN_POINT('Ctrl Pts',(-0.0786793252660694,-0.452457377108644,
0.340789283404409));
#43364=CARTESIAN_POINT('Ctrl Pts',(-0.10322605317072,-0.447736883397827,
0.339969902788797));
#43365=CARTESIAN_POINT('Ctrl Pts',(-0.123810173907499,-0.443778424540985,
0.339282795750064));
#43366=CARTESIAN_POINT('Ctrl Pts',(-0.144122638314188,-0.43848000679386,
0.338597263743002));
#43367=CARTESIAN_POINT('Ctrl Pts',(-0.164009324183141,-0.431848940441746,
0.337911670583885));
#43368=CARTESIAN_POINT('Ctrl Pts',(-0.173238698931143,-0.428771474606271,
0.337593488045484));
#43369=CARTESIAN_POINT('Ctrl Pts',(-0.182376275359539,-0.425406617445509,
0.337275292335719));
#43370=CARTESIAN_POINT('Ctrl Pts',(-0.191405887931006,-0.421753266829663,
0.3369569199004));
#43371=CARTESIAN_POINT('Ctrl Pts',(-0.196618434355552,-0.419644288228475,
0.336773132269838));
#43372=CARTESIAN_POINT('Ctrl Pts',(-0.201785860418484,-0.417442838008913,
0.336589607391786));
#43373=CARTESIAN_POINT('Ctrl Pts',(-0.206905131052897,-0.415149652617678,
0.336406322902213));
#43374=CARTESIAN_POINT('Ctrl Pts',(-0.230173294793032,-0.404726641806129,
0.335573256276322));
#43375=CARTESIAN_POINT('Ctrl Pts',(-0.252449394294505,-0.392412097418436,
0.334745101295834));
#43376=CARTESIAN_POINT('Ctrl Pts',(-0.273462988147765,-0.378233667265445,
0.333919012981835));
#43377=CARTESIAN_POINT('Ctrl Pts',(-0.288822939436902,-0.367869899980937,
0.333315181178852));
#43378=CARTESIAN_POINT('Ctrl Pts',(-0.303508291533758,-0.356509065180283,
0.332712453580099));
#43379=CARTESIAN_POINT('Ctrl Pts',(-0.317480036993706,-0.344248782374799,
0.332109719099858));
#43380=CARTESIAN_POINT('Ctrl Pts',(-0.32442200017635,-0.338157171839205,
0.331810246096808));
#43381=CARTESIAN_POINT('Ctrl Pts',(-0.331187642820478,-0.331843302499605,
0.331510771394944));
#43382=CARTESIAN_POINT('Ctrl Pts',(-0.337771160258578,-0.325318048159448,
0.331211158711015));
#43383=CARTESIAN_POINT('Ctrl Pts',(-0.34183643772567,-0.321288747761068,
0.331026149906181));
#43384=CARTESIAN_POINT('Ctrl Pts',(-0.345831067083111,-0.317179806234212,
0.330841137997783));
#43385=CARTESIAN_POINT('Ctrl Pts',(-0.349745720442196,-0.313002903467174,
0.330656479407013));
#43386=CARTESIAN_POINT('Ctrl Pts',(-0.366864224643312,-0.294737601023669,
0.329848980358718));
#43387=CARTESIAN_POINT('Ctrl Pts',(-0.382500655113849,-0.275132445206135,
0.329046214584533));
#43388=CARTESIAN_POINT('Ctrl Pts',(-0.396573125796599,-0.254434970524844,
0.328245596979643));
#43389=CARTESIAN_POINT('Ctrl Pts',(-0.40930334920357,-0.235711643072761,
0.327521343136549));
#43390=CARTESIAN_POINT('Ctrl Pts',(-0.420753757249109,-0.216093166297332,
0.326798847216462));
#43391=CARTESIAN_POINT('Ctrl Pts',(-0.430837734643622,-0.19573929488211,
0.326076195513572));
#43392=CARTESIAN_POINT('Ctrl Pts',(-0.434459892094156,-0.188428198862203,
0.325816619539989));
#43393=CARTESIAN_POINT('Ctrl Pts',(-0.437905483329181,-0.181022066702969,
0.325557023466667));
#43394=CARTESIAN_POINT('Ctrl Pts',(-0.441169547255124,-0.173527888906457,
0.325297318602195));
#43395=CARTESIAN_POINT('Ctrl Pts',(-0.443252573854766,-0.168745331932464,
0.325131582834445));
#43396=CARTESIAN_POINT('Ctrl Pts',(-0.445260942161103,-0.163928315057075,
0.324965852626416));
#43397=CARTESIAN_POINT('Ctrl Pts',(-0.447190162062795,-0.159087569551048,
0.324800404574383));
#43398=CARTESIAN_POINT('Ctrl Pts',(-0.456742756959829,-0.135118461219655,
0.323981183180187));
#43399=CARTESIAN_POINT('Ctrl Pts',(-0.464384303051498,-0.110511230558558,
0.323166844164823));
#43400=CARTESIAN_POINT('Ctrl Pts',(-0.470005652087834,-0.0855055059985193,
0.322354690199387));
#43401=CARTESIAN_POINT('Ctrl Pts',(-0.475490118350773,-0.0611086838401096,
0.321562312605512));
#43402=CARTESIAN_POINT('Ctrl Pts',(-0.479052081018164,-0.0363312413003476,
0.320772014942982));
#43403=CARTESIAN_POINT('Ctrl Pts',(-0.480543654488575,-0.0113809312581294,
0.319981292167799));
#43404=CARTESIAN_POINT('Ctrl Pts',(-0.480771456586696,-0.0075703693990342,
0.319860528215642));
#43405=CARTESIAN_POINT('Ctrl Pts',(-0.480950867488915,-0.0037557678692382,
0.31973975434763));
#43406=CARTESIAN_POINT('Ctrl Pts',(-0.481081249970215,6.21355392569225E-5,
0.319618961639866));
#43407=CARTESIAN_POINT('',(0.0697955034108395,0.486863953835044,0.3075));
#43408=CARTESIAN_POINT('Ctrl Pts',(0.0698314663893227,0.486747372427084,
0.3075));
#43409=CARTESIAN_POINT('Ctrl Pts',(0.0442470650552309,0.487370644859313,
0.310410073119928));
#43410=CARTESIAN_POINT('Ctrl Pts',(0.018704409302911,0.48608015899137,0.313334011041929));
#43411=CARTESIAN_POINT('Ctrl Pts',(-0.00656009088084865,0.482874809315394,
0.316282658377337));
#43412=CARTESIAN_POINT('Ctrl Pts',(-0.0255467494552765,0.480465939974351,
0.318498611980479));
#43413=CARTESIAN_POINT('Ctrl Pts',(-0.0443764046829174,0.476974515955641,
0.320728520848864));
#43414=CARTESIAN_POINT('Ctrl Pts',(-0.0629406504805546,0.472382319692998,
0.322976987839482));
#43415=CARTESIAN_POINT('Ctrl Pts',(-0.0730547215737834,0.469880424384095,
0.324201985355771));
#43416=CARTESIAN_POINT('Ctrl Pts',(-0.0830898537740494,0.467051537608078,
0.325432491347468));
#43417=CARTESIAN_POINT('Ctrl Pts',(-0.0930270499457564,0.463890934176298,
0.326669250158342));
#43418=CARTESIAN_POINT('Ctrl Pts',(-0.0990188180630417,0.461985205181247,
0.327414970770446));
#43419=CARTESIAN_POINT('Ctrl Pts',(-0.104975897972382,0.459958313281541,
0.328163094796111));
#43420=CARTESIAN_POINT('Ctrl Pts',(-0.110878233577805,0.457815290850395,
0.328911766032642));
#43421=CARTESIAN_POINT('Ctrl Pts',(-0.133573530023649,0.449575073313414,
0.331790510446621));
#43422=CARTESIAN_POINT('Ctrl Pts',(-0.155517947173888,0.439604362330888,
0.334684288072021));
#43423=CARTESIAN_POINT('Ctrl Pts',(-0.176494052666361,0.427876171853613,
0.337603770956938));
#43424=CARTESIAN_POINT('Ctrl Pts',(-0.178064691351246,0.426997994077767,
0.337822374584792));
#43425=CARTESIAN_POINT('Ctrl Pts',(-0.179629886094255,0.426109943451997,
0.338041122332846));
#43426=CARTESIAN_POINT('Ctrl Pts',(-0.181189537858252,0.425211999409135,
0.338260018681348));
#43427=CARTESIAN_POINT('Ctrl Pts',(-0.196947491648197,0.416139614752499,
0.340471639649637));
#43428=CARTESIAN_POINT('Ctrl Pts',(-0.212140744926486,0.406057980777516,
0.34269842988097));
#43429=CARTESIAN_POINT('Ctrl Pts',(-0.226690439368773,0.395046192060306,
0.34494501019069));
#43430=CARTESIAN_POINT('Ctrl Pts',(-0.233632026251567,0.389792522409806,
0.346016842487303));
#43431=CARTESIAN_POINT('Ctrl Pts',(-0.240426924417161,0.384327011933825,
0.347093179394951));
#43432=CARTESIAN_POINT('Ctrl Pts',(-0.247065363968451,0.378657760718284,
0.348174522716671));
#43433=CARTESIAN_POINT('Ctrl Pts',(-0.252478394053154,0.374035013587674,
0.349056257631501));
#43434=CARTESIAN_POINT('Ctrl Pts',(-0.257789430726446,0.369274532028075,
0.349941703414435));
#43435=CARTESIAN_POINT('Ctrl Pts',(-0.262975387221713,0.364397963208855,
0.350828068454723));
#43436=CARTESIAN_POINT('Ctrl Pts',(-0.280204713927883,0.348196516577331,
0.353772843034685));
#43437=CARTESIAN_POINT('Ctrl Pts',(-0.296100249356768,0.330680913403001,
0.356734624194827));
#43438=CARTESIAN_POINT('Ctrl Pts',(-0.310500746304381,0.312039737428418,
0.359725026866486));
#43439=CARTESIAN_POINT('Ctrl Pts',(-0.319875678890449,0.299904061227625,
0.361671822421804));
#43440=CARTESIAN_POINT('Ctrl Pts',(-0.328616148097658,0.287290689006832,
0.363630748343365));
#43441=CARTESIAN_POINT('Ctrl Pts',(-0.33666630465908,0.274247977633762,
0.365605009340675));
#43442=CARTESIAN_POINT('Ctrl Pts',(-0.342961754433943,0.264048209001847,
0.367148937195519));
#43443=CARTESIAN_POINT('Ctrl Pts',(-0.3488348232303,0.253585792876292,0.368702243494569));
#43444=CARTESIAN_POINT('Ctrl Pts',(-0.354267090617469,0.242885040692727,
0.370266460933668));
#43445=CARTESIAN_POINT('Ctrl Pts',(-0.356941497389496,0.237616860379455,
0.371036554416534));
#43446=CARTESIAN_POINT('Ctrl Pts',(-0.359509312395157,0.2322898014544,0.37180944552389));
#43447=CARTESIAN_POINT('Ctrl Pts',(-0.361961446378714,0.226922541435087,
0.372583073900236));
#43448=CARTESIAN_POINT('Ctrl Pts',(-0.37140492256759,0.20625254846906,0.375562414017882));
#43449=CARTESIAN_POINT('Ctrl Pts',(-0.379164540226144,0.184934471292981,
0.378560389293445));
#43450=CARTESIAN_POINT('Ctrl Pts',(-0.385152715128125,0.163143884177883,
0.381589261171817));
#43451=CARTESIAN_POINT('Ctrl Pts',(-0.390990790306795,0.141899500396909,
0.384542211281314));
#43452=CARTESIAN_POINT('Ctrl Pts',(-0.395145084054741,0.120204809722708,
0.387524528496279));
#43453=CARTESIAN_POINT('Ctrl Pts',(-0.397485650378386,0.098227288615696,
0.390547575143355));
#43454=CARTESIAN_POINT('Ctrl Pts',(-0.39810341816627,0.0924265537848513,
0.391345476412364));
#43455=CARTESIAN_POINT('Ctrl Pts',(-0.398594566690346,0.0866061945215394,
0.392146215057885));
#43456=CARTESIAN_POINT('Ctrl Pts',(-0.398956125446125,0.0807695020971151,
0.39295));
#43457=CARTESIAN_POINT('',(-0.342664481608845,0.353895656000097,0.3075));
#43458=CARTESIAN_POINT('Origin',(0.,0.,0.3075));
#43459=CARTESIAN_POINT('Ctrl Pts',(-0.481081249970215,6.21355392569225E-5,
0.319618961639866));
#43460=CARTESIAN_POINT('Ctrl Pts',(-0.481245905746716,0.00488364103652631,
0.319466416475099));
#43461=CARTESIAN_POINT('Ctrl Pts',(-0.481332358526736,0.00971269744067388,
0.319313769100939));
#43462=CARTESIAN_POINT('Ctrl Pts',(-0.481339290728969,0.0145394320803265,
0.319161266227293));
#43463=CARTESIAN_POINT('Ctrl Pts',(-0.481374927233973,0.0393523194386921,
0.318377291779119));
#43464=CARTESIAN_POINT('Ctrl Pts',(-0.479315765619102,0.0640754382249796,
0.317598006650885));
#43465=CARTESIAN_POINT('Ctrl Pts',(-0.475334185366473,0.0885133909011413,
0.316821056278798));
#43466=CARTESIAN_POINT('Ctrl Pts',(-0.471321611003206,0.113141577745898,
0.316038057834271));
#43467=CARTESIAN_POINT('Ctrl Pts',(-0.465356080254756,0.137481253645947,
0.315257430636602));
#43468=CARTESIAN_POINT('Ctrl Pts',(-0.457563909950549,0.161331853653742,
0.314476764706437));
#43469=CARTESIAN_POINT('Ctrl Pts',(-0.454530796981434,0.170615732391066,
0.314172889423314));
#43470=CARTESIAN_POINT('Ctrl Pts',(-0.45122042339318,0.179825411865552,
0.313869008271574));
#43471=CARTESIAN_POINT('Ctrl Pts',(-0.447638452480909,0.188948473220082,
0.313564979115321));
#43472=CARTESIAN_POINT('Ctrl Pts',(-0.445471137905168,0.194468491202731,
0.313381022618203));
#43473=CARTESIAN_POINT('Ctrl Pts',(-0.443204366528429,0.199956368985501,
0.313197024052677));
#43474=CARTESIAN_POINT('Ctrl Pts',(-0.440845177239491,0.20539685797324,
0.31301337682937));
#43475=CARTESIAN_POINT('Ctrl Pts',(-0.430431121133819,0.229412547526533,
0.312202711701251));
#43476=CARTESIAN_POINT('Ctrl Pts',(-0.418196042282852,0.252569544019692,
0.311396773420503));
#43477=CARTESIAN_POINT('Ctrl Pts',(-0.404292000940336,0.274648614567846,
0.310592949274326));
#43478=CARTESIAN_POINT('Ctrl Pts',(-0.390460558173166,0.296612401434999,
0.309793322216349));
#43479=CARTESIAN_POINT('Ctrl Pts',(-0.374976844053069,0.317510780436166,
0.308995787273091));
#43480=CARTESIAN_POINT('Ctrl Pts',(-0.357945478548728,0.337105770246179,
0.308197772444498));
#43481=CARTESIAN_POINT('Ctrl Pts',(-0.352982808855556,0.342815439388291,
0.307965243584522));
#43482=CARTESIAN_POINT('Ctrl Pts',(-0.347888479690135,0.34841423125597,
0.307732673980019));
#43483=CARTESIAN_POINT('Ctrl Pts',(-0.342664481608845,0.353895656000097,
0.3075));
#43484=CARTESIAN_POINT('',(-0.4,-4.89858719658941E-17,0.4));
#43485=CARTESIAN_POINT('',(-0.45,-5.51091059616309E-17,0.35));
#43486=CARTESIAN_POINT('Origin',(0.,0.,0.4));
#43487=CARTESIAN_POINT('Ctrl Pts',(0.285821514250018,-0.401076441581685,
-0.0493345805022535));
#43488=CARTESIAN_POINT('Ctrl Pts',(0.350543656524979,-0.354953112478679,
-0.0454821295218614));
#43489=CARTESIAN_POINT('Ctrl Pts',(0.456341900696097,-0.230941845013787,
-0.037777227561077));
#43490=CARTESIAN_POINT('Ctrl Pts',(0.532545219900247,0.0886035482833393,
-0.0223674236395085));
#43491=CARTESIAN_POINT('Ctrl Pts',(0.319330773560668,0.47994453109398,-0.00310516873754761));
#43492=CARTESIAN_POINT('Ctrl Pts',(-0.215290254258889,0.535025635481654,
0.0200095371448053));
#43493=CARTESIAN_POINT('Ctrl Pts',(-0.562384412092527,0.125896602679806,
0.0431242430271583));
#43494=CARTESIAN_POINT('Ctrl Pts',(-0.422683627229176,-0.392004271488446,
0.0662389489095112));
#43495=CARTESIAN_POINT('Ctrl Pts',(0.0835198470635792,-0.570404842180615,
0.0893536547918642));
#43496=CARTESIAN_POINT('Ctrl Pts',(0.517219798545357,-0.254477109971328,
0.112468360674217));
#43497=CARTESIAN_POINT('Ctrl Pts',(0.502837016033576,0.281900700313858,
0.13558306655657));
#43498=CARTESIAN_POINT('Ctrl Pts',(0.0527054858386194,0.574051566754687,
0.158697772438923));
#43499=CARTESIAN_POINT('Ctrl Pts',(-0.44304232133121,0.368766078993326,
0.181812478321276));
#43500=CARTESIAN_POINT('Ctrl Pts',(-0.554979510632384,-0.155996767962851,
0.204927184203629));
#43501=CARTESIAN_POINT('Ctrl Pts',(-0.185906336843711,-0.545680887986882,
0.228041890085982));
#43502=CARTESIAN_POINT('Ctrl Pts',(0.343997419455209,-0.462376423424824,
0.251156595968335));
#43503=CARTESIAN_POINT('Ctrl Pts',(0.576325602595985,0.0212396797004994,
0.274271301850687));
#43504=CARTESIAN_POINT('Ctrl Pts',(0.308311929055428,0.487096140686821,
0.297386007733041));
#43505=CARTESIAN_POINT('Ctrl Pts',(-0.135936610051597,0.522471279645762,
0.316648262635001));
#43506=CARTESIAN_POINT('Ctrl Pts',(-0.396756348714945,0.322748301101158,
0.33205806655657));
#43507=CARTESIAN_POINT('Ctrl Pts',(-0.466937021208664,0.175620002884023,
0.339762968517355));
#43508=CARTESIAN_POINT('Ctrl Pts',(-0.482707018258731,0.0977250455296118,
0.343615419497747));
#43509=CARTESIAN_POINT('Ctrl Pts',(0.269291261530787,-0.377880514723374,
-0.0328897203348357));
#43510=CARTESIAN_POINT('Ctrl Pts',(0.330270251821047,-0.334424690508254,
-0.0290372693544436));
#43511=CARTESIAN_POINT('Ctrl Pts',(0.429949741363115,-0.217585512928218,
-0.0213323673936592));
#43512=CARTESIAN_POINT('Ctrl Pts',(0.501745904136811,0.083479234780252,
-0.00592256347209064));
#43513=CARTESIAN_POINT('Ctrl Pts',(0.300862540328343,0.452187333001269,
0.0133396914298702));
#43514=CARTESIAN_POINT('Ctrl Pts',(-0.202839119080262,0.504082866918604,
0.0364543973122232));
#43515=CARTESIAN_POINT('Ctrl Pts',(-0.529859371135975,0.118615475979983,
0.0595691031945761));
#43516=CARTESIAN_POINT('Ctrl Pts',(-0.398238066520727,-0.369333026142464,
0.0826838090769291));
#43517=CARTESIAN_POINT('Ctrl Pts',(0.0786895452486333,-0.537415946231828,
0.105798514959282));
#43518=CARTESIAN_POINT('Ctrl Pts',(0.487306815949282,-0.23975963515099,
0.128913220841635));
#43519=CARTESIAN_POINT('Ctrl Pts',(0.473755849860941,0.265597204651036,
0.152027926723988));
#43520=CARTESIAN_POINT('Ctrl Pts',(0.0496573073175292,0.540851765482816,
0.175142632606341));
#43521=CARTESIAN_POINT('Ctrl Pts',(-0.417419332256589,0.347438795440041,
0.198257338488694));
#43522=CARTESIAN_POINT('Ctrl Pts',(-0.522882726074999,-0.146974822905372,
0.221372044371047));
#43523=CARTESIAN_POINT('Ctrl Pts',(-0.175154596415085,-0.51412188163935,
0.2444867502534));
#43524=CARTESIAN_POINT('Ctrl Pts',(0.324102611000083,-0.435635262422014,
0.267601456135753));
#43525=CARTESIAN_POINT('Ctrl Pts',(0.542994284327405,0.0200113002552149,
0.290716162018105));
#43526=CARTESIAN_POINT('Ctrl Pts',(0.290480961652527,0.458925335122226,
0.313830867900458));
#43527=CARTESIAN_POINT('Ctrl Pts',(-0.128074827764688,0.492254581949836,
0.333093122802419));
#43528=CARTESIAN_POINT('Ctrl Pts',(-0.373810270882328,0.3040824179681,0.348502926723988));
#43529=CARTESIAN_POINT('Ctrl Pts',(-0.439932101775649,0.165463164138548,
0.356207828684772));
#43530=CARTESIAN_POINT('Ctrl Pts',(-0.454790053987863,0.0920731977187791,
0.360060279665165));
#43531=CARTESIAN_POINT('Ctrl Pts',(0.252761008811555,-0.354684587865062,
-0.0164448601674179));
#43532=CARTESIAN_POINT('Ctrl Pts',(0.309996847117115,-0.313896268537829,
-0.0125924091870257));
#43533=CARTESIAN_POINT('Ctrl Pts',(0.403557582030132,-0.204229180842649,
-0.00488750722624137));
#43534=CARTESIAN_POINT('Ctrl Pts',(0.470946588373376,0.0783549212771649,
0.0105222966953272));
#43535=CARTESIAN_POINT('Ctrl Pts',(0.282394307096019,0.424430134908558,
0.029784551597288));
#43536=CARTESIAN_POINT('Ctrl Pts',(-0.190387983901635,0.473140098355552,
0.052899257479641));
#43537=CARTESIAN_POINT('Ctrl Pts',(-0.497334330179422,0.111334349280159,
0.076013963361994));
#43538=CARTESIAN_POINT('Ctrl Pts',(-0.373792505812278,-0.346661780796483,
0.0991286692443469));
#43539=CARTESIAN_POINT('Ctrl Pts',(0.0738592434336875,-0.50442705028304,
0.1222433751267));
#43540=CARTESIAN_POINT('Ctrl Pts',(0.457393833353206,-0.225042160330651,
0.145358081009053));
#43541=CARTESIAN_POINT('Ctrl Pts',(0.444674683688306,0.249293708988214,
0.168472786891406));
#43542=CARTESIAN_POINT('Ctrl Pts',(0.0466091287964395,0.507651964210947,
0.191587492773759));
#43543=CARTESIAN_POINT('Ctrl Pts',(-0.391796343181968,0.326111511886755,
0.214702198656111));
#43544=CARTESIAN_POINT('Ctrl Pts',(-0.490785941517614,-0.137952877847892,
0.237816904538465));
#43545=CARTESIAN_POINT('Ctrl Pts',(-0.164402855986459,-0.482562875291818,
0.260931610420817));
#43546=CARTESIAN_POINT('Ctrl Pts',(0.304207802544958,-0.408894101419205,
0.28404631630317));
#43547=CARTESIAN_POINT('Ctrl Pts',(0.509662966058825,0.0187829208099306,
0.307161022185524));
#43548=CARTESIAN_POINT('Ctrl Pts',(0.272649994249626,0.430754529557631,
0.330275728067876));
#43549=CARTESIAN_POINT('Ctrl Pts',(-0.120213045477778,0.46203788425391,
0.349537982969837));
#43550=CARTESIAN_POINT('Ctrl Pts',(-0.350864193049711,0.285416534835041,
0.364947786891406));
#43551=CARTESIAN_POINT('Ctrl Pts',(-0.412927182342633,0.155306325393072,
0.37265268885219));
#43552=CARTESIAN_POINT('Ctrl Pts',(-0.426873089716994,0.0864213499079464,
0.376505139832582));
#43553=CARTESIAN_POINT('Ctrl Pts',(0.236230756092324,-0.331488661006751,
-5.55111512312578E-17));
#43554=CARTESIAN_POINT('Ctrl Pts',(0.289723442413183,-0.293367846567404,
0.00385245098039209));
#43555=CARTESIAN_POINT('Ctrl Pts',(0.37716542269715,-0.19087284875708,0.0115573529411765));
#43556=CARTESIAN_POINT('Ctrl Pts',(0.44014727260994,0.0732306077740779,
0.026967156862745));
#43557=CARTESIAN_POINT('Ctrl Pts',(0.263926073863695,0.396672936815846,
0.0462294117647059));
#43558=CARTESIAN_POINT('Ctrl Pts',(-0.177936848723007,0.442197329792502,
0.0693441176470588));
#43559=CARTESIAN_POINT('Ctrl Pts',(-0.46480928922287,0.104053222580335,
0.0924588235294117));
#43560=CARTESIAN_POINT('Ctrl Pts',(-0.349346945103829,-0.323990535450501,
0.115573529411765));
#43561=CARTESIAN_POINT('Ctrl Pts',(0.0690289416187412,-0.471438154334252,
0.138688235294118));
#43562=CARTESIAN_POINT('Ctrl Pts',(0.427480850757132,-0.210324685510313,
0.161802941176471));
#43563=CARTESIAN_POINT('Ctrl Pts',(0.41559351751567,0.232990213325393,0.184917647058823));
#43564=CARTESIAN_POINT('Ctrl Pts',(0.0435609502753498,0.474452162939076,
0.208032352941177));
#43565=CARTESIAN_POINT('Ctrl Pts',(-0.366173354107348,0.304784228333469,
0.231147058823529));
#43566=CARTESIAN_POINT('Ctrl Pts',(-0.458689156960228,-0.128930932790413,
0.254261764705883));
#43567=CARTESIAN_POINT('Ctrl Pts',(-0.153651115557833,-0.451003868944285,
0.277376470588235));
#43568=CARTESIAN_POINT('Ctrl Pts',(0.284312994089833,-0.382152940416395,
0.300491176470589));
#43569=CARTESIAN_POINT('Ctrl Pts',(0.476331647790245,0.0175545413646465,
0.323605882352941));
#43570=CARTESIAN_POINT('Ctrl Pts',(0.254819026846725,0.402583723993036,
0.346720588235294));
#43571=CARTESIAN_POINT('Ctrl Pts',(-0.112351263190869,0.431821186557985,
0.365982843137255));
#43572=CARTESIAN_POINT('Ctrl Pts',(-0.327918115217093,0.266750651701983,
0.381392647058824));
#43573=CARTESIAN_POINT('Ctrl Pts',(-0.385922262909618,0.145149486647597,
0.389097549019608));
#43574=CARTESIAN_POINT('Ctrl Pts',(-0.398956125446125,0.0807695020971137,
0.39295));
#43575=CARTESIAN_POINT('',(0.236230756092325,-0.331488661006751,0.));
#43576=CARTESIAN_POINT('Ctrl Pts',(0.236230756092324,-0.331488661006751,
-5.55111512312578E-17));
#43577=CARTESIAN_POINT('Ctrl Pts',(0.289723442413183,-0.293367846567404,
0.00385245098039209));
#43578=CARTESIAN_POINT('Ctrl Pts',(0.37716542269715,-0.19087284875708,0.0115573529411765));
#43579=CARTESIAN_POINT('Ctrl Pts',(0.44014727260994,0.0732306077740779,
0.026967156862745));
#43580=CARTESIAN_POINT('Ctrl Pts',(0.263926073863695,0.396672936815846,
0.0462294117647059));
#43581=CARTESIAN_POINT('Ctrl Pts',(-0.177936848723007,0.442197329792502,
0.0693441176470588));
#43582=CARTESIAN_POINT('Ctrl Pts',(-0.390945071629489,0.191118922825079,
0.0865072247563608));
#43583=CARTESIAN_POINT('Ctrl Pts',(-0.407283047524291,0.0301769837418441,
0.0959654299048784));
#43584=CARTESIAN_POINT('Ctrl Pts',(-0.407034641531608,0.000294318473894748,
0.0977187330926118));
#43585=CARTESIAN_POINT('Ctrl Pts',(0.217447815076512,0.442338803773993,
-3.8597597340484E-17));
#43586=CARTESIAN_POINT('Ctrl Pts',(0.235771185649973,0.431537188392035,
-4.42054783740276E-17));
#43587=CARTESIAN_POINT('Ctrl Pts',(0.253300690580711,0.419546382573851,
-1.43244558183068E-17));
#43588=CARTESIAN_POINT('Ctrl Pts',(0.269890299702997,0.406369790209568,
2.16840434497101E-17));
#43589=CARTESIAN_POINT('Ctrl Pts',(0.281071263833339,0.397489110411798,
4.87538430948304E-17));
#43590=CARTESIAN_POINT('Ctrl Pts',(0.291824924692404,0.388069292305422,
-6.77184820252973E-17));
#43591=CARTESIAN_POINT('Ctrl Pts',(0.30213264706158,0.37815074175771,-7.80625564189563E-17));
#43592=CARTESIAN_POINT('Ctrl Pts',(0.30776728830288,0.372728838453719,-8.37170692292625E-17));
#43593=CARTESIAN_POINT('Ctrl Pts',(0.313270261594427,0.367156075512075,
1.65417925227048E-18));
#43594=CARTESIAN_POINT('Ctrl Pts',(0.318632624766842,0.361444505503272,
-7.80625564189563E-18));
#43595=CARTESIAN_POINT('Ctrl Pts',(0.336033064429788,0.342910917582537,
-3.85046103165619E-17));
#43596=CARTESIAN_POINT('Ctrl Pts',(0.351905028805777,0.322974626561441,
-8.88307993243271E-18));
#43597=CARTESIAN_POINT('Ctrl Pts',(0.366150538251326,0.301871858897891,
3.46944695195361E-17));
#43598=CARTESIAN_POINT('Ctrl Pts',(0.372568420276111,0.292364647254896,
5.4327012138036E-17));
#43599=CARTESIAN_POINT('Ctrl Pts',(0.37865556572648,0.282620326083274,3.4499532893746E-17));
#43600=CARTESIAN_POINT('Ctrl Pts',(0.384399785951081,0.272659327527138,
5.89805981832114E-17));
#43601=CARTESIAN_POINT('Ctrl Pts',(0.388480791465398,0.265582494041263,
7.6373274392731E-17));
#43602=CARTESIAN_POINT('Ctrl Pts',(0.392390160301114,0.25839280128157,2.53748915853478E-17));
#43603=CARTESIAN_POINT('Ctrl Pts',(0.396111438865062,0.251121487239994,
2.25514051876985E-17));
#43604=CARTESIAN_POINT('Ctrl Pts',(0.40745358116902,0.228959137074835,1.39456574681695E-17));
#43605=CARTESIAN_POINT('Ctrl Pts',(0.417077210155165,0.205999660918854,
-8.66004344781302E-17));
#43606=CARTESIAN_POINT('Ctrl Pts',(0.424881751749804,0.182459781868829,
-6.93889390390723E-17));
#43607=CARTESIAN_POINT('Ctrl Pts',(0.430607845296002,0.165188870070598,
-5.6761082327833E-17));
#43608=CARTESIAN_POINT('Ctrl Pts',(0.435353796515255,0.147604950608036,
7.4600576781502E-17));
#43609=CARTESIAN_POINT('Ctrl Pts',(0.439061990731694,0.129792158612379,
1.00613961606655E-16));
#43610=CARTESIAN_POINT('Ctrl Pts',(0.441052023831415,0.120232776443923,
1.14574259750785E-16));
#43611=CARTESIAN_POINT('Ctrl Pts',(0.442742911254792,0.11060749250059,6.5499624826844E-17));
#43612=CARTESIAN_POINT('Ctrl Pts',(0.444123791797554,0.100929672122365,
6.24500451351651E-17));
#43613=CARTESIAN_POINT('Ctrl Pts',(0.445088133438485,0.094171140232625,
6.03203629556022E-17));
#43614=CARTESIAN_POINT('Ctrl Pts',(0.445901192054133,0.087385117597804,
9.07916038813422E-17));
#43615=CARTESIAN_POINT('Ctrl Pts',(0.446557500931817,0.0805979169647933,
8.32667268468867E-17));
#43616=CARTESIAN_POINT('Ctrl Pts',(0.448915348394345,0.056214300752433,
5.62329431745785E-17));
#43617=CARTESIAN_POINT('Ctrl Pts',(0.449264882015899,0.0317529871848161,
2.53752424620923E-17));
#43618=CARTESIAN_POINT('Ctrl Pts',(0.447476027996775,0.00742372749985042,
2.77555756156289E-17));
#43619=CARTESIAN_POINT('Ctrl Pts',(0.446180524189214,-0.0101957362574197,
2.94794338123863E-17));
#43620=CARTESIAN_POINT('Ctrl Pts',(0.443762029056545,-0.0277461199319404,
4.3074745668937E-17));
#43621=CARTESIAN_POINT('Ctrl Pts',(0.440260086235777,-0.045127533989719,
5.55111512312578E-17));
#43622=CARTESIAN_POINT('Ctrl Pts',(0.438497782445595,-0.0538744877352476,
6.17695985504835E-17));
#43623=CARTESIAN_POINT('Ctrl Pts',(0.436460883233537,-0.0625785391661663,
4.81993018880041E-17));
#43624=CARTESIAN_POINT('Ctrl Pts',(0.434153233316401,-0.0712260787334543,
5.55111512312578E-17));
#43625=CARTESIAN_POINT('Ctrl Pts',(0.432455960374384,-0.0775863306995747,
6.08890051051305E-17));
#43626=CARTESIAN_POINT('Ctrl Pts',(0.43061151612711,-0.0839173798140132,
-1.92100666488577E-17));
#43627=CARTESIAN_POINT('Ctrl Pts',(0.42862810433969,-0.0901940790812472,
-1.38777878078145E-17));
#43628=CARTESIAN_POINT('Ctrl Pts',(0.421563946478226,-0.112549292836608,
5.11375985434415E-18));
#43629=CARTESIAN_POINT('Ctrl Pts',(0.412726164773691,-0.134275543420596,
-3.59125272893349E-17));
#43630=CARTESIAN_POINT('Ctrl Pts',(0.402223235339076,-0.155144150016548,
-2.08166817117217E-17));
#43631=CARTESIAN_POINT('Ctrl Pts',(0.395782695443094,-0.16794106483841,
-1.15597028553478E-17));
#43632=CARTESIAN_POINT('Ctrl Pts',(0.388715069443995,-0.18041506830769,
9.54523787347189E-17));
#43633=CARTESIAN_POINT('Ctrl Pts',(0.381038025471632,-0.192507033808116,
9.71445146547012E-17));
#43634=CARTESIAN_POINT('Ctrl Pts',(0.374554680793545,-0.202718826323181,
9.88257224754246E-17));
#43635=CARTESIAN_POINT('Ctrl Pts',(0.367636567228464,-0.212658063476375,
4.58363829752519E-17));
#43636=CARTESIAN_POINT('Ctrl Pts',(0.360298753602303,-0.222297236750623,
4.16333634234434E-17));
#43637=CARTESIAN_POINT('Ctrl Pts',(0.356885786025934,-0.226780613887746,
3.96784528487154E-17));
#43638=CARTESIAN_POINT('Ctrl Pts',(0.353381726209429,-0.231199059390674,
-6.35056968455181E-17));
#43639=CARTESIAN_POINT('Ctrl Pts',(0.349797863823796,-0.235538458422797,
-6.24500451351651E-17));
#43640=CARTESIAN_POINT('Ctrl Pts',(0.335312213365481,-0.253077920270008,
-5.81831955643792E-17));
#43641=CARTESIAN_POINT('Ctrl Pts',(0.319489163245678,-0.269378119582282,
-1.177990700976E-17));
#43642=CARTESIAN_POINT('Ctrl Pts',(0.302455374280317,-0.284284251770872,
-3.46944695195361E-17));
#43643=CARTESIAN_POINT('Ctrl Pts',(0.285837815097629,-0.298826144612952,
-5.70491023863626E-17));
#43644=CARTESIAN_POINT('Ctrl Pts',(0.268066931012482,-0.312041854936447,
1.51086484203379E-17));
#43645=CARTESIAN_POINT('Ctrl Pts',(0.249239140885698,-0.323743396449302,
0.));
#43646=CARTESIAN_POINT('Ctrl Pts',(0.244957374879624,-0.326404529929706,
-3.43596868077925E-18));
#43647=CARTESIAN_POINT('Ctrl Pts',(0.240620893760326,-0.32898714764827,
-1.20546207527071E-17));
#43648=CARTESIAN_POINT('Ctrl Pts',(0.236230756092325,-0.331488661006751,
-1.38777878078145E-17));
#43649=CARTESIAN_POINT('Ctrl Pts',(0.0698314663893245,0.486747372427084,
0.3075));
#43650=CARTESIAN_POINT('Ctrl Pts',(0.13882856656482,0.47715546868819,0.304128669244347));
#43651=CARTESIAN_POINT('Ctrl Pts',(0.20570919792813,0.453597245499616,0.300757338488694));
#43652=CARTESIAN_POINT('Ctrl Pts',(0.264131166824116,0.416528424980888,
0.297386007733041));
#43653=CARTESIAN_POINT('Ctrl Pts',(0.397649820235614,0.33181065369138,0.289681105772257));
#43654=CARTESIAN_POINT('Ctrl Pts',(0.486987711415799,0.17652516669594,0.281976203811472));
#43655=CARTESIAN_POINT('Ctrl Pts',(0.492935293149096,0.0182797393439991,
0.274271301850688));
#43656=CARTESIAN_POINT('Ctrl Pts',(0.498882874882393,-0.139965688007942,
0.266566399889903));
#43657=CARTESIAN_POINT('Ctrl Pts',(0.421440147168801,-0.301171055716382,
0.258861497929119));
#43658=CARTESIAN_POINT('Ctrl Pts',(0.294401490595519,-0.395657816997613,
0.251156595968335));
#43659=CARTESIAN_POINT('Ctrl Pts',(0.167362834022236,-0.490144578278843,
0.243451694007551));
#43660=CARTESIAN_POINT('Ctrl Pts',(-0.00927175141073788,-0.517912733132863,
0.235746792046766));
#43661=CARTESIAN_POINT('Ctrl Pts',(-0.15910123975867,-0.466849457222534,
0.228041890085982));
#43662=CARTESIAN_POINT('Ctrl Pts',(-0.308930728106602,-0.415786181312205,
0.220336988125198));
#43663=CARTESIAN_POINT('Ctrl Pts',(-0.431955119369493,-0.285891474637528,
0.212632086164413));
#43664=CARTESIAN_POINT('Ctrl Pts',(-0.474811116784076,-0.133483646807493,
0.204927184203629));
#43665=CARTESIAN_POINT('Ctrl Pts',(-0.486942274642154,-0.0903418806661754,
0.202746173665872));
#43666=CARTESIAN_POINT('Ctrl Pts',(-0.492649743945157,-0.0453961956515631,
0.200565163128115));
#43667=CARTESIAN_POINT('Ctrl Pts',(-0.492300964172325,-0.000364928074014725,
0.198384152590358));
#43668=CARTESIAN_POINT('Origin',(0.,0.,-0.277281266907388));
#43669=CARTESIAN_POINT('',(-0.236771598461275,-0.331576719094244,-5.03775273800896E-17));
#43670=CARTESIAN_POINT('Ctrl Pts',(-0.236771598461276,-0.331576719094244,
-2.30935062739412E-17));
#43671=CARTESIAN_POINT('Ctrl Pts',(-0.141722621809602,-0.398300946144845,
0.00683327564849024));
#43672=CARTESIAN_POINT('Ctrl Pts',(0.126781614045834,-0.452218967011808,
0.0214259299022832));
#43673=CARTESIAN_POINT('Ctrl Pts',(0.447438415353507,-0.166418058771462,
0.0437779627613788));
#43674=CARTESIAN_POINT('Ctrl Pts',(0.389000999211174,0.276972659072313,
0.067056098577287));
#43675=CARTESIAN_POINT('Ctrl Pts',(-0.0110871576621449,0.477410398031793,
0.0903342343931949));
#43676=CARTESIAN_POINT('Ctrl Pts',(-0.347644687561783,0.288793871360888,
0.110409290503229));
#43677=CARTESIAN_POINT('Ctrl Pts',(-0.406221861873601,0.0777548455075631,
0.12272496800796));
#43678=CARTESIAN_POINT('Ctrl Pts',(-0.406522025929715,-0.000167002740521567,
0.127281266907388));
#43679=CARTESIAN_POINT('Origin',(0.,0.,0.));
#43680=CARTESIAN_POINT('Ctrl Pts',(-0.179217368492184,0.36547344271607,
-0.0493345805022535));
#43681=CARTESIAN_POINT('Ctrl Pts',(-0.238611205238638,0.336348461575858,
-0.0454548911996022));
#43682=CARTESIAN_POINT('Ctrl Pts',(-0.342150032955443,0.248603248616071,
-0.0376955125942995));
#43683=CARTESIAN_POINT('Ctrl Pts',(-0.44676970066958,-0.00417527992601634,
-0.0221767553836941));
#43684=CARTESIAN_POINT('Ctrl Pts',(-0.320810106679502,-0.353702698155029,
-0.00277830887043734));
#43685=CARTESIAN_POINT('Ctrl Pts',(0.113495967335977,-0.464060443259162,
0.0204998269454708));
#43686=CARTESIAN_POINT('Ctrl Pts',(0.447438415353507,-0.166418058771462,
0.0437779627613788));
#43687=CARTESIAN_POINT('Ctrl Pts',(0.389000999211174,0.276972659072313,
0.067056098577287));
#43688=CARTESIAN_POINT('Ctrl Pts',(-0.0110871576621449,0.477410398031793,
0.0903342343931949));
#43689=CARTESIAN_POINT('Ctrl Pts',(-0.401344193454667,0.258699122660778,
0.113612370209103));
#43690=CARTESIAN_POINT('Ctrl Pts',(-0.439359289932517,-0.187051465698632,
0.136890506025011));
#43691=CARTESIAN_POINT('Ctrl Pts',(-0.0916847062669661,-0.468629856473293,
0.160168641840919));
#43692=CARTESIAN_POINT('Ctrl Pts',(0.336453410254844,-0.338849716643417,
0.183446777656827));
#43693=CARTESIAN_POINT('Ctrl Pts',(0.46926975494663,0.088378354603048,0.206724913472736));
#43694=CARTESIAN_POINT('Ctrl Pts',(0.190156376929569,0.437998801366229,
0.230003049288643));
#43695=CARTESIAN_POINT('Ctrl Pts',(-0.255854007963939,0.403215004461254,
0.253281185104552));
#43696=CARTESIAN_POINT('Ctrl Pts',(-0.477314526631585,0.0143692006508807,
0.27655932092046));
#43697=CARTESIAN_POINT('Ctrl Pts',(-0.279730339285618,-0.386842400859151,
0.299837456736368));
#43698=CARTESIAN_POINT('Ctrl Pts',(0.163268921903001,-0.448972926511222,
0.323115592552276));
#43699=CARTESIAN_POINT('Ctrl Pts',(0.463203848138002,-0.116047052095292,
0.346393728368184));
#43700=CARTESIAN_POINT('Ctrl Pts',(0.373893623429547,0.244589772389548,
0.365792174881441));
#43701=CARTESIAN_POINT('Ctrl Pts',(0.146530577079214,0.396735441137677,
0.381310932092046));
#43702=CARTESIAN_POINT('Ctrl Pts',(0.0116987864547665,0.412224129892184,
0.389070310697349));
#43703=CARTESIAN_POINT('Ctrl Pts',(-0.0538698874795526,0.403469624287802,
0.39295));
#43704=CARTESIAN_POINT('Ctrl Pts',(-0.191758108071807,0.391047455474608,
-0.0328897203348357));
#43705=CARTESIAN_POINT('Ctrl Pts',(-0.255308029942927,0.359884453093409,
-0.0290100310321843));
#43706=CARTESIAN_POINT('Ctrl Pts',(-0.366091989566869,0.265999266790941,
-0.0212506524268816));
#43707=CARTESIAN_POINT('Ctrl Pts',(-0.478032420992403,-0.00446744523713975,
-0.00573189521627628));
#43708=CARTESIAN_POINT('Ctrl Pts',(-0.343258801447355,-0.378453052785785,
0.0136665512969805));
#43709=CARTESIAN_POINT('Ctrl Pts',(0.121437850322391,-0.496533083701774,
0.0369446871128886));
#43710=CARTESIAN_POINT('Ctrl Pts',(0.478747929002081,-0.178063166352039,
0.0602228229287966));
#43711=CARTESIAN_POINT('Ctrl Pts',(0.416221353289375,0.296353827411771,
0.0835009587447048));
#43712=CARTESIAN_POINT('Ctrl Pts',(-0.0118629817805825,0.510817201873923,
0.106779094560613));
#43713=CARTESIAN_POINT('Ctrl Pts',(-0.429428262840657,0.276801599859618,
0.130057230376521));
#43714=CARTESIAN_POINT('Ctrl Pts',(-0.470103466589548,-0.200140396414718,
0.153335366192429));
#43715=CARTESIAN_POINT('Ctrl Pts',(-0.098100345746565,-0.501422241713142,
0.176613502008337));
#43716=CARTESIAN_POINT('Ctrl Pts',(0.359996745558678,-0.362560733543208,
0.199891637824245));
#43717=CARTESIAN_POINT('Ctrl Pts',(0.502106917097217,0.0945626320471215,
0.223169773640153));
#43718=CARTESIAN_POINT('Ctrl Pts',(0.203462573882139,0.468647777803804,
0.246447909456061));
#43719=CARTESIAN_POINT('Ctrl Pts',(-0.273757398194884,0.431429983891475,
0.269726045271969));
#43720=CARTESIAN_POINT('Ctrl Pts',(-0.510714621870228,0.0153746858047257,
0.293004181087878));
#43721=CARTESIAN_POINT('Ctrl Pts',(-0.299304476362928,-0.413911706966848,
0.316282316903785));
#43722=CARTESIAN_POINT('Ctrl Pts',(0.174693668557066,-0.480389817614186,
0.339560452719694));
#43723=CARTESIAN_POINT('Ctrl Pts',(0.495616548316844,-0.1241674472978,0.362838588535602));
#43724=CARTESIAN_POINT('Ctrl Pts',(0.400056838531749,0.261704947470977,
0.382237035048858));
#43725=CARTESIAN_POINT('Ctrl Pts',(0.156784057660157,0.42449701297178,0.397755792259464));
#43726=CARTESIAN_POINT('Ctrl Pts',(0.0125174093123678,0.441069523086539,
0.405515170864767));
#43727=CARTESIAN_POINT('Ctrl Pts',(-0.0576394341242136,0.43170242074638,
0.409394860167418));
#43728=CARTESIAN_POINT('Ctrl Pts',(-0.20429884765143,0.416621468233146,
-0.0164448601674178));
#43729=CARTESIAN_POINT('Ctrl Pts',(-0.272004854647215,0.38342044461096,
-0.0125651708647665));
#43730=CARTESIAN_POINT('Ctrl Pts',(-0.390033946178295,0.283395284965812,
-0.00480579225946384));
#43731=CARTESIAN_POINT('Ctrl Pts',(-0.509295141315226,-0.00475961054826249,
0.0107129649511416));
#43732=CARTESIAN_POINT('Ctrl Pts',(-0.365707496215208,-0.403203407416541,
0.0301114114643983));
#43733=CARTESIAN_POINT('Ctrl Pts',(0.129379733308805,-0.529005724144386,
0.0533895472803064));
#43734=CARTESIAN_POINT('Ctrl Pts',(0.510057442650656,-0.189708273932616,
0.0766676830962145));
#43735=CARTESIAN_POINT('Ctrl Pts',(0.443441707367576,0.315734995751229,
0.0999458189121226));
#43736=CARTESIAN_POINT('Ctrl Pts',(-0.0126388058990205,0.544224005716052,
0.123223954728031));
#43737=CARTESIAN_POINT('Ctrl Pts',(-0.457512332226647,0.294904077058458,
0.146502090543939));
#43738=CARTESIAN_POINT('Ctrl Pts',(-0.500847643246579,-0.213229327130804,
0.169780226359847));
#43739=CARTESIAN_POINT('Ctrl Pts',(-0.104515985226164,-0.534214626952992,
0.193058362175755));
#43740=CARTESIAN_POINT('Ctrl Pts',(0.383540080862511,-0.386271750443,0.216336497991663));
#43741=CARTESIAN_POINT('Ctrl Pts',(0.534944079247805,0.100746909491195,
0.239614633807571));
#43742=CARTESIAN_POINT('Ctrl Pts',(0.21676877083471,0.499296754241378,0.262892769623479));
#43743=CARTESIAN_POINT('Ctrl Pts',(-0.291660788425829,0.459644963321696,
0.286170905439387));
#43744=CARTESIAN_POINT('Ctrl Pts',(-0.544114717108871,0.0163801709585708,
0.309449041255295));
#43745=CARTESIAN_POINT('Ctrl Pts',(-0.318878613440237,-0.440981013074545,
0.332727177071203));
#43746=CARTESIAN_POINT('Ctrl Pts',(0.186118415211131,-0.511806708717149,
0.356005312887112));
#43747=CARTESIAN_POINT('Ctrl Pts',(0.528029248495686,-0.132287842500309,
0.37928344870302));
#43748=CARTESIAN_POINT('Ctrl Pts',(0.426220053633952,0.278820122552406,
0.398681895216276));
#43749=CARTESIAN_POINT('Ctrl Pts',(0.167037538241101,0.452258584805883,
0.414200652426882));
#43750=CARTESIAN_POINT('Ctrl Pts',(0.0133360321699692,0.469914916280895,
0.421960031032184));
#43751=CARTESIAN_POINT('Ctrl Pts',(-0.0614089807688746,0.459935217204959,
0.425839720334836));
#43752=CARTESIAN_POINT('Ctrl Pts',(-0.216839587231054,0.442195480991683,
0.));
#43753=CARTESIAN_POINT('Ctrl Pts',(-0.288701679351503,0.406956436128511,
0.00387968930265134));
#43754=CARTESIAN_POINT('Ctrl Pts',(-0.413975902789721,0.300791303140682,
0.011639067907954));
#43755=CARTESIAN_POINT('Ctrl Pts',(-0.54055786163805,-0.00505177585938594,
0.0271578251185594));
#43756=CARTESIAN_POINT('Ctrl Pts',(-0.38815619098306,-0.427953762047296,
0.0465562716318161));
#43757=CARTESIAN_POINT('Ctrl Pts',(0.137321616295219,-0.561478364586998,
0.0698344074477243));
#43758=CARTESIAN_POINT('Ctrl Pts',(0.541366956299231,-0.201353381513192,
0.0931125432636322));
#43759=CARTESIAN_POINT('Ctrl Pts',(0.470662061445776,0.335116164090687,
0.11639067907954));
#43760=CARTESIAN_POINT('Ctrl Pts',(-0.0134146300174581,0.577630809558183,
0.139668814895449));
#43761=CARTESIAN_POINT('Ctrl Pts',(-0.485596401612636,0.313006554257298,
0.162946950711356));
#43762=CARTESIAN_POINT('Ctrl Pts',(-0.53159181990361,-0.226318257846889,
0.186225086527265));
#43763=CARTESIAN_POINT('Ctrl Pts',(-0.110931624705763,-0.567007012192843,
0.209503222343173));
#43764=CARTESIAN_POINT('Ctrl Pts',(0.407083416166345,-0.409982767342791,
0.232781358159081));
#43765=CARTESIAN_POINT('Ctrl Pts',(0.567781241398392,0.106931186935269,
0.256059493974989));
#43766=CARTESIAN_POINT('Ctrl Pts',(0.230074967787281,0.529945730678953,
0.279337629790897));
#43767=CARTESIAN_POINT('Ctrl Pts',(-0.309564178656774,0.487859942751916,
0.302615765606805));
#43768=CARTESIAN_POINT('Ctrl Pts',(-0.577514812347514,0.0173856561124158,
0.325893901422713));
#43769=CARTESIAN_POINT('Ctrl Pts',(-0.338452750517546,-0.468050319182243,
0.349172037238622));
#43770=CARTESIAN_POINT('Ctrl Pts',(0.197543161865195,-0.543223599820112,
0.372450173054529));
#43771=CARTESIAN_POINT('Ctrl Pts',(0.560441948674527,-0.140408237702817,
0.395728308870437));
#43772=CARTESIAN_POINT('Ctrl Pts',(0.452383268736155,0.295935297633835,
0.415126755383694));
#43773=CARTESIAN_POINT('Ctrl Pts',(0.177291018822044,0.480020156639985,
0.4306455125943));
#43774=CARTESIAN_POINT('Ctrl Pts',(0.0141546550275704,0.49876030947525,
0.438404891199602));
#43775=CARTESIAN_POINT('Ctrl Pts',(-0.0651785274135356,0.488168013663537,
0.442284580502254));
#43776=CARTESIAN_POINT('Ctrl Pts',(-0.491861190935719,-0.000202060802622812,
0.176615847409642));
#43777=CARTESIAN_POINT('Ctrl Pts',(-0.492116503801431,-0.0664806507023142,
0.179818927115516));
#43778=CARTESIAN_POINT('Ctrl Pts',(-0.479592887105073,-0.13266715951835,
0.18302200682139));
#43779=CARTESIAN_POINT('Ctrl Pts',(-0.45381588432214,-0.193212248220517,
0.186225086527265));
#43780=CARTESIAN_POINT('Ctrl Pts',(-0.391371754837661,-0.339881175962207,
0.193984465132567));
#43781=CARTESIAN_POINT('Ctrl Pts',(-0.251151689771712,-0.453444094077525,
0.20174384373787));
#43782=CARTESIAN_POINT('Ctrl Pts',(-0.0947058170933862,-0.484054845660175,
0.209503222343173));
#43783=CARTESIAN_POINT('Ctrl Pts',(0.0617400555849396,-0.514665597242825,
0.217262600948475));
#43784=CARTESIAN_POINT('Ctrl Pts',(0.234411735875642,-0.462324182292808,
0.225021979553778));
#43785=CARTESIAN_POINT('Ctrl Pts',(0.347530546893001,-0.35000114910479,
0.232781358159081));
#43786=CARTESIAN_POINT('Ctrl Pts',(0.46064935791036,-0.237678115916771,
0.240540736764384));
#43787=CARTESIAN_POINT('Ctrl Pts',(0.514215299654376,-0.0653734644907513,
0.248300115369686));
#43788=CARTESIAN_POINT('Ctrl Pts',(0.484713891591199,0.0912812851795395,
0.256059493974989));
#43789=CARTESIAN_POINT('Ctrl Pts',(0.455212483528021,0.24793603484983,0.263818872580292));
#43790=CARTESIAN_POINT('Ctrl Pts',(0.342643725657651,0.388940882764392,
0.271578251185594));
#43791=CARTESIAN_POINT('Ctrl Pts',(0.19641948898179,0.452429008733833,0.279337629790897));
#43792=CARTESIAN_POINT('Ctrl Pts',(0.0501952523059287,0.515917134703274,
0.2870970083962));
#43793=CARTESIAN_POINT('Ctrl Pts',(-0.129684463175423,0.501888538727595,
0.294856387001502));
#43794=CARTESIAN_POINT('Ctrl Pts',(-0.264282759864555,0.416461859633172,
0.302615765606805));
#43795=CARTESIAN_POINT('Ctrl Pts',(-0.292524266622378,0.398537575342149,
0.30424384373787));
#43796=CARTESIAN_POINT('Ctrl Pts',(-0.318772271610817,0.377470010455589,
0.305871921868935));
#43797=CARTESIAN_POINT('Ctrl Pts',(-0.342664481608841,0.353895656000101,
0.3075));
#43798=CARTESIAN_POINT('Ctrl Pts',(-0.236771598461275,-0.331576719094244,
1.77809156287623E-17));
#43799=CARTESIAN_POINT('Ctrl Pts',(-0.250685093761403,-0.323785106371382,
1.80035313947998E-17));
#43800=CARTESIAN_POINT('Ctrl Pts',(-0.264074236959953,-0.315173418978676,
2.94409432717802E-17));
#43801=CARTESIAN_POINT('Ctrl Pts',(-0.276852406183546,-0.305762684301697,
2.29850860566927E-17));
#43802=CARTESIAN_POINT('Ctrl Pts',(-0.287822209380187,-0.297683756441541,
1.72958474292146E-17));
#43803=CARTESIAN_POINT('Ctrl Pts',(-0.298341885321039,-0.289015772946681,
3.86197526290172E-17));
#43804=CARTESIAN_POINT('Ctrl Pts',(-0.308399583438957,-0.27981147161853,
4.68375338513738E-17));
#43805=CARTESIAN_POINT('Ctrl Pts',(-0.313176580152552,-0.275439803600658,
5.07406450237306E-17));
#43806=CARTESIAN_POINT('Ctrl Pts',(-0.317849715293028,-0.270946637032549,
2.78009939264429E-17));
#43807=CARTESIAN_POINT('Ctrl Pts',(-0.322416173250408,-0.266338360354402,
3.55618312575245E-17));
#43808=CARTESIAN_POINT('Ctrl Pts',(-0.338339031391128,-0.250269683821266,
6.26232239232097E-17));
#43809=CARTESIAN_POINT('Ctrl Pts',(-0.352891345987932,-0.232881717338864,
-2.29443486208257E-18));
#43810=CARTESIAN_POINT('Ctrl Pts',(-0.366023507015969,-0.214414045295771,
2.25514051876985E-17));
#43811=CARTESIAN_POINT('Ctrl Pts',(-0.372915048500564,-0.204722515642947,
3.55900921987028E-17));
#43812=CARTESIAN_POINT('Ctrl Pts',(-0.379415068568767,-0.194732824866228,
9.50689841530354E-17));
#43813=CARTESIAN_POINT('Ctrl Pts',(-0.385513091657106,-0.184475102093045,
8.15320033709099E-17));
#43814=CARTESIAN_POINT('Ctrl Pts',(-0.38870776678985,-0.179101214295747,
7.4440154873356E-17));
#43815=CARTESIAN_POINT('Ctrl Pts',(-0.391791940744699,-0.17365352637825,
7.3696258065194E-17));
#43816=CARTESIAN_POINT('Ctrl Pts',(-0.394757285743178,-0.168149505204942,
6.93889390390723E-17));
#43817=CARTESIAN_POINT('Ctrl Pts',(-0.406042481613924,-0.147202884474678,
5.29966005717066E-17));
#43818=CARTESIAN_POINT('Ctrl Pts',(-0.415636815927215,-0.12539890172167,
1.40125039712718E-17));
#43819=CARTESIAN_POINT('Ctrl Pts',(-0.423478528957865,-0.102985404860791,
2.77555756156289E-17));
#43820=CARTESIAN_POINT('Ctrl Pts',(-0.429376839283599,-0.0861266191014051,
3.80927176495664E-17));
#43821=CARTESIAN_POINT('Ctrl Pts',(-0.434283049989256,-0.0689218306178823,
5.65608473286771E-17));
#43822=CARTESIAN_POINT('Ctrl Pts',(-0.43815575437846,-0.0514644871269222,
4.5102810375397E-17));
#43823=CARTESIAN_POINT('Ctrl Pts',(-0.439906400633787,-0.0435729390150655,
3.99232336585234E-17));
#43824=CARTESIAN_POINT('Ctrl Pts',(-0.44144565613257,-0.0356296777440409,
6.15140867947257E-17));
#43825=CARTESIAN_POINT('Ctrl Pts',(-0.442768644909789,-0.0276429456528638,
5.89805981832114E-17));
#43826=CARTESIAN_POINT('Ctrl Pts',(-0.443871289745052,-0.0209864047640719,
5.68690624084653E-17));
#43827=CARTESIAN_POINT('Ctrl Pts',(-0.44482365403208,-0.0142978621335312,
3.1313155957869E-17));
#43828=CARTESIAN_POINT('Ctrl Pts',(-0.445620686304564,-0.00760396509680276,
3.81639164714898E-17));
#43829=CARTESIAN_POINT('Ctrl Pts',(-0.448419947719333,0.015905707392318,
6.22245100379753E-17));
#43830=CARTESIAN_POINT('Ctrl Pts',(-0.449317353814376,0.039538445055359,
1.16772899686138E-16));
#43831=CARTESIAN_POINT('Ctrl Pts',(-0.44823656490343,0.0630780692117099,
1.04083408558608E-16));
#43832=CARTESIAN_POINT('Ctrl Pts',(-0.447374340120413,0.081857358233785,
9.47489001442916E-17));
#43833=CARTESIAN_POINT('Ctrl Pts',(-0.445252620327562,0.100578184059543,
7.52302054080897E-18));
#43834=CARTESIAN_POINT('Ctrl Pts',(-0.441939735912287,0.119138777262726,
-6.93889390390723E-18));
#43835=CARTESIAN_POINT('Ctrl Pts',(-0.440350972534721,0.128039899985618,
-1.38744090499585E-17));
#43836=CARTESIAN_POINT('Ctrl Pts',(-0.438487949296401,0.136904200117995,
7.29844862664086E-17));
#43837=CARTESIAN_POINT('Ctrl Pts',(-0.436356577222032,0.145720408589059,
7.28583859910259E-17));
#43838=CARTESIAN_POINT('Ctrl Pts',(-0.434687913405322,0.152622670401133,
7.27596613387989E-17));
#43839=CARTESIAN_POINT('Ctrl Pts',(-0.43285383314019,0.159497658516508,
1.23405815283735E-18));
#43840=CARTESIAN_POINT('Ctrl Pts',(-0.430864188011168,0.166317151368737,
0.));
#43841=CARTESIAN_POINT('Ctrl Pts',(-0.423921464110642,0.190113282308881,
-4.30615736814992E-18));
#43842=CARTESIAN_POINT('Ctrl Pts',(-0.415075878758636,0.213293450260572,
-2.85677649743916E-17));
#43843=CARTESIAN_POINT('Ctrl Pts',(-0.404491724583964,0.235635990622313,
-2.08166817117217E-17));
#43844=CARTESIAN_POINT('Ctrl Pts',(-0.397747393951119,0.249872884462906,
-1.5877612663459E-17));
#43845=CARTESIAN_POINT('Ctrl Pts',(-0.390295993937811,0.263769868300252,
5.84132300429329E-17));
#43846=CARTESIAN_POINT('Ctrl Pts',(-0.382169143027842,0.277268407825058,
6.93889390390723E-17));
#43847=CARTESIAN_POINT('Ctrl Pts',(-0.375587981126775,0.288199588306262,
7.8277119551156E-17));
#43848=CARTESIAN_POINT('Ctrl Pts',(-0.368563698892631,0.298869479267404,
6.83778588982247E-18));
#43849=CARTESIAN_POINT('Ctrl Pts',(-0.36111404718269,0.309257673710277,
-6.93889390390723E-18));
#43850=CARTESIAN_POINT('Ctrl Pts',(-0.356830943331032,0.315230263753738,
-1.4859660214209E-17));
#43851=CARTESIAN_POINT('Ctrl Pts',(-0.352405080449604,0.32111196869177,
8.37777440281965E-17));
#43852=CARTESIAN_POINT('Ctrl Pts',(-0.347855489317613,0.326879369584256,
8.32667268468867E-17));
#43853=CARTESIAN_POINT('Ctrl Pts',(-0.332050949477965,0.346914382518844,
8.14915362492162E-17));
#43854=CARTESIAN_POINT('Ctrl Pts',(-0.314723541600508,0.365621295399423,
6.08259975105604E-18));
#43855=CARTESIAN_POINT('Ctrl Pts',(-0.296050162210069,0.382860211578897,
2.08166817117217E-17));
#43856=CARTESIAN_POINT('Ctrl Pts',(-0.277394780843452,0.400082512317878,
3.55365624743834E-17));
#43857=CARTESIAN_POINT('Ctrl Pts',(-0.257395271430084,0.415840722974244,
5.73069542662832E-17));
#43858=CARTESIAN_POINT('Ctrl Pts',(-0.236184952673479,0.429968144128177,
6.24500451351651E-17));
#43859=CARTESIAN_POINT('Ctrl Pts',(-0.229843975137141,0.434191638419397,
6.39876091878868E-17));
#43860=CARTESIAN_POINT('Ctrl Pts',(-0.223394530553168,0.43826913492392,
3.92474881692199E-17));
#43861=CARTESIAN_POINT('Ctrl Pts',(-0.216839587231054,0.442195480991683,
4.16333634234434E-17));
#43862=CARTESIAN_POINT('Origin',(0.,0.,0.));
#43863=CARTESIAN_POINT('Origin',(-0.144337567297407,-0.25,-0.2));
#43864=CARTESIAN_POINT('',(-0.144337567297407,-0.25,-0.2));
#43865=CARTESIAN_POINT('',(0.144337567297406,-0.25,-0.2));
#43866=CARTESIAN_POINT('',(-0.0721687836487033,-0.25,-0.2));
#43867=CARTESIAN_POINT('',(-0.144337567297407,-0.25,-0.1));
#43868=CARTESIAN_POINT('',(-0.144337567297407,-0.25,-0.2));
#43869=CARTESIAN_POINT('',(0.144337567297406,-0.25,-0.1));
#43870=CARTESIAN_POINT('',(-0.144337567297407,-0.25,-0.1));
#43871=CARTESIAN_POINT('',(0.144337567297406,-0.25,-0.2));
#43872=CARTESIAN_POINT('Origin',(-0.288675134594813,3.53525079574969E-17,
-0.2));
#43873=CARTESIAN_POINT('',(-0.288675134594813,3.53525079574969E-17,-0.2));
#43874=CARTESIAN_POINT('',(-0.252590742770461,-0.0625,-0.2));
#43875=CARTESIAN_POINT('',(-0.288675134594813,5.55111512312578E-17,-0.1));
#43876=CARTESIAN_POINT('',(-0.288675134594813,3.53525079574969E-17,-0.2));
#43877=CARTESIAN_POINT('',(-0.288675134594813,3.53525079574969E-17,-0.1));
#43878=CARTESIAN_POINT('Origin',(-0.144337567297406,0.25,-0.2));
#43879=CARTESIAN_POINT('',(-0.144337567297406,0.25,-0.2));
#43880=CARTESIAN_POINT('',(-0.180421959121758,0.1875,-0.2));
#43881=CARTESIAN_POINT('',(-0.144337567297406,0.25,-0.1));
#43882=CARTESIAN_POINT('',(-0.144337567297406,0.25,-0.2));
#43883=CARTESIAN_POINT('',(-0.144337567297406,0.25,-0.1));
#43884=CARTESIAN_POINT('Origin',(0.144337567297406,0.25,-0.2));
#43885=CARTESIAN_POINT('',(0.144337567297406,0.25,-0.2));
#43886=CARTESIAN_POINT('',(0.0721687836487033,0.25,-0.2));
#43887=CARTESIAN_POINT('',(0.144337567297406,0.25,-0.1));
#43888=CARTESIAN_POINT('',(0.144337567297406,0.25,-0.2));
#43889=CARTESIAN_POINT('',(0.144337567297406,0.25,-0.1));
#43890=CARTESIAN_POINT('Origin',(0.288675134594813,0.,-0.2));
#43891=CARTESIAN_POINT('',(0.288675134594813,0.,-0.2));
#43892=CARTESIAN_POINT('',(0.252590742770461,0.0625,-0.2));
#43893=CARTESIAN_POINT('',(0.288675134594813,0.,-0.1));
#43894=CARTESIAN_POINT('',(0.288675134594813,0.,-0.2));
#43895=CARTESIAN_POINT('',(0.288675134594813,0.,-0.1));
#43896=CARTESIAN_POINT('Origin',(0.144337567297406,-0.25,-0.2));
#43897=CARTESIAN_POINT('',(0.180421959121758,-0.1875,-0.2));
#43898=CARTESIAN_POINT('',(0.144337567297406,-0.25,-0.1));
#43899=CARTESIAN_POINT('Origin',(0.,0.,-0.1));
#43900=CARTESIAN_POINT('Origin',(0.,0.,0.));
#43901=CARTESIAN_POINT('',(-0.6,-7.34788079488412E-17,0.));
#43902=CARTESIAN_POINT('Origin',(0.,0.,0.));
#43903=CARTESIAN_POINT('Origin',(0.,0.,-0.2));
#43904=CARTESIAN_POINT('',(-0.6,-7.34788079488412E-17,-0.2));
#43905=CARTESIAN_POINT('',(-0.6,-7.34788079488412E-17,-0.2));
#43906=CARTESIAN_POINT('Origin',(0.,0.,-0.2));
#43907=CARTESIAN_POINT('Origin',(0.,0.,-0.2));
#43908=CARTESIAN_POINT('Origin',(0.,0.,0.4));
#43960=UNCERTAINTY_MEASURE_WITH_UNIT(LENGTH_MEASURE(0.001),#43981,
'DISTANCE_ACCURACY_VALUE',
'Maximum model space distance between geometric entities at asserted c
onnectivities');
#43961=UNCERTAINTY_MEASURE_WITH_UNIT(LENGTH_MEASURE(0.001),#43981,
'DISTANCE_ACCURACY_VALUE',
'Maximum model space distance between geometric entities at asserted c
onnectivities');
#43979=(
GEOMETRIC_REPRESENTATION_CONTEXT(3)
GLOBAL_UNCERTAINTY_ASSIGNED_CONTEXT((#43960))
GLOBAL_UNIT_ASSIGNED_CONTEXT((#43981,#43983,#43984))
REPRESENTATION_CONTEXT('','3D')
);
#43980=(
GEOMETRIC_REPRESENTATION_CONTEXT(3)
GLOBAL_UNCERTAINTY_ASSIGNED_CONTEXT((#43961))
GLOBAL_UNIT_ASSIGNED_CONTEXT((#43981,#43983,#43984))
REPRESENTATION_CONTEXT('','3D')
);
#43981=(
LENGTH_UNIT()
NAMED_UNIT(*)
SI_UNIT(.CENTI.,.METRE.)
);
#43983=(
NAMED_UNIT(*)
PLANE_ANGLE_UNIT()
SI_UNIT($,.RADIAN.)
);
#43984=(
NAMED_UNIT(*)
SI_UNIT($,.STERADIAN.)
SOLID_ANGLE_UNIT()
);
#44002=SHAPE_DEFINITION_REPRESENTATION(#44020,#44072);
#44020=PRODUCT_DEFINITION_SHAPE('',$,#44091);
#44072=SHAPE_REPRESENTATION('',(#12207),#43979);
#44073=PRODUCT_DEFINITION_CONTEXT('part definition',#44129,'design');
#44091=PRODUCT_DEFINITION('Socket head cap screw M10x4',
'Socket head cap screw M10x4',#44109,#44073);
#44109=PRODUCT_DEFINITION_FORMATION('',$,#44148);
#44129=APPLICATION_CONTEXT(
'Core Data for Automotive Mechanical Design Process');
#44130=PRODUCT_CONTEXT('part definition',#44129,'mechanical');
#44148=PRODUCT('Socket head cap screw M10x4',
'Socket head cap screw M10x4',$,(#44130));
#44160=PRESENTATION_STYLE_ASSIGNMENT((#44172));
#44172=SURFACE_STYLE_USAGE(.BOTH.,#44184);
#44184=SURFACE_SIDE_STYLE('',(#44196));
#44196=SURFACE_STYLE_FILL_AREA(#44208);
#44208=FILL_AREA_STYLE('Dark gray',(#44220));
#44220=FILL_AREA_STYLE_COLOUR('Dark gray',#44232);
#44232=COLOUR_RGB('Dark gray',0.250980392156863,0.282352941176471,0.32156862745098);
ENDSEC;
END-ISO-10303-21;
